ISO-10303-21;
HEADER;
FILE_DESCRIPTION (('STEP AP203'),
    '1' );
FILE_NAME ('bench vise-.step',
    '2026-10-07T23:37:23',
    ( '' ),
    ( '' ),
    'SwSTEP 2.0',
    'SolidWorks 2024',
    '' );
FILE_SCHEMA (( 'AUTOMOTIVE_DESIGN' ));
ENDSEC;

DATA;
#9=CARTESIAN_POINT ( 'NONE',  ( -8.751021560936518753E-10, 1.365923996832131609E-16, 5.750408897959578548E-10 ) ) ;
#12=PLANE ( 'NONE',  #8081 ) ;
#16=CARTESIAN_POINT ( 'NONE',  ( 3.544128228010244186, 1.000000000000000000, 1.972857804739797549 ) ) ;
#25=VECTOR ( 'NONE', #5396, 39.37007874015748143 ) ;
#26=DIRECTION ( 'NONE',  ( -0.000000000000000000, -1.000000000000000000, -0.000000000000000000 ) ) ;
#39=AXIS2_PLACEMENT_3D ( 'NONE', #7359, #1153, #8008 ) ;
#48=AXIS2_PLACEMENT_3D ( 'NONE', #4004, #7908, #4660 ) ;
#51=FACE_BOUND ( 'NONE', #4197, .T. ) ;
#53=PLANE ( 'NONE',  #82 ) ;
#54=ORIENTED_EDGE ( 'NONE', *, *, #6929, .T. ) ;
#61=ADVANCED_FACE ( 'NONE', ( #5673, #1333, #92, #2030, #51, #5721 ), #132, .F. ) ;
#66=DIRECTION ( 'NONE',  ( 2.664535259084986204E-15, 0.000000000000000000, 1.000000000000000000 ) ) ;
#80=ORIENTED_EDGE ( 'NONE', *, *, #6042, .T. ) ;
#82=AXIS2_PLACEMENT_3D ( 'NONE', #2571, #5061, #7600 ) ;
#86=ORIENTED_EDGE ( 'NONE', *, *, #479, .F. ) ;
#89=DIRECTION ( 'NONE',  ( 0.9917930140014037388, -0.000000000000000000, 0.1278538907425633420 ) ) ;
#92=FACE_BOUND ( 'NONE', #7637, .T. ) ;
#97=LINE ( 'NONE', #5064, #3478 ) ;
#107=CARTESIAN_POINT ( 'NONE',  ( -8.751021560936518753E-10, 1.365923996832131609E-16, 5.750408897959578548E-10 ) ) ;
#111=ORIENTED_EDGE ( 'NONE', *, *, #1410, .F. ) ;
#129=ADVANCED_FACE ( 'NONE', ( #841 ), #1421, .F. ) ;
#132=PLANE ( 'NONE',  #3078 ) ;
#147=DIRECTION ( 'NONE',  ( 0.000000000000000000, -1.000000000000000000, 0.000000000000000000 ) ) ;
#148=ORIENTED_EDGE ( 'NONE', *, *, #4983, .T. ) ;
#153=ORIENTED_EDGE ( 'NONE', *, *, #632, .T. ) ;
#157=DIRECTION ( 'NONE',  ( 0.000000000000000000, -0.000000000000000000, 1.000000000000000000 ) ) ;
#166=EDGE_CURVE ( 'NONE', #7244, #3899, #2692, .T. ) ;
#174=ORIENTED_EDGE ( 'NONE', *, *, #2746, .F. ) ;
#178=CARTESIAN_POINT ( 'NONE',  ( -8.751021560936518753E-10, 1.365923996832131609E-16, 5.750408897959578548E-10 ) ) ;
#180=AXIS2_PLACEMENT_3D ( 'NONE', #661, #26, #4591 ) ;
#181=VECTOR ( 'NONE', #6775, 39.37007874015748143 ) ;
#184=ORIENTED_EDGE ( 'NONE', *, *, #6285, .F. ) ;
#191=VECTOR ( 'NONE', #2428, 39.37007874015748854 ) ;
#194=CARTESIAN_POINT ( 'NONE',  ( 1.674765980421384803, 1.000000000000000444, -3.533905825348209628 ) ) ;
#213=PLANE ( 'NONE',  #3235 ) ;
#229=DIRECTION ( 'NONE',  ( -0.000000000000000000, 1.000000000000000000, 0.000000000000000000 ) ) ;
#233=FACE_OUTER_BOUND ( 'NONE', #3987, .T. ) ;
#258=ORIENTED_EDGE ( 'NONE', *, *, #926, .T. ) ;
#261=CARTESIAN_POINT ( 'NONE',  ( 3.562500000000000444, 0.000000000000000000, 2.612499999999998934 ) ) ;
#269=DIRECTION ( 'NONE',  ( -0.08785522361217638909, 0.000000000000000000, 0.9961332539796342589 ) ) ;
#270=ORIENTED_EDGE ( 'NONE', *, *, #7587, .T. ) ;
#275=CARTESIAN_POINT ( 'NONE',  ( 3.762484563843161212, 1.281112611882646579, -9.215429355903707278E-16 ) ) ;
#276=ADVANCED_FACE ( 'NONE', ( #7465 ), #2741, .F. ) ;
#295=VERTEX_POINT ( 'NONE', #6301 ) ;
#299=CARTESIAN_POINT ( 'NONE',  ( -1.172489671586610660, 1.365923996832131609E-16, -3.693357951819909779 ) ) ;
#317=EDGE_CURVE ( 'NONE', #3161, #1533, #4107, .T. ) ;
#322=PLANE ( 'NONE',  #719 ) ;
#325=ORIENTED_EDGE ( 'NONE', *, *, #5751, .T. ) ;
#342=AXIS2_PLACEMENT_3D ( 'NONE', #4778, #1515, #3551 ) ;
#355=ORIENTED_EDGE ( 'NONE', *, *, #2044, .F. ) ;
#362=LINE ( 'NONE', #7823, #7425 ) ;
#365=EDGE_LOOP ( 'NONE', ( #474, #3997, #3213, #6406 ) ) ;
#375=ORIENTED_EDGE ( 'NONE', *, *, #2486, .T. ) ;
#380=DIRECTION ( 'NONE',  ( 0.000000000000000000, 0.000000000000000000, -1.000000000000000000 ) ) ;
#385=ORIENTED_EDGE ( 'NONE', *, *, #7050, .T. ) ;
#388=EDGE_CURVE ( 'NONE', #6365, #3479, #3288, .T. ) ;
#392=DIRECTION ( 'NONE',  ( -0.000000000000000000, -1.000000000000000000, -0.000000000000000000 ) ) ;
#400=CARTESIAN_POINT ( 'NONE',  ( -8.751021560936518753E-10, 1.365923996832131609E-16, 5.750408897959578548E-10 ) ) ;
#415=CARTESIAN_POINT ( 'NONE',  ( 3.796513186599488776, 1.365923996832131609E-16, -2.946478861041413211 ) ) ;
#425=ADVANCED_FACE ( 'NONE', ( #5050 ), #1169, .F. ) ;
#427=CARTESIAN_POINT ( 'NONE',  ( -8.751021560936518753E-10, 1.365923996832131609E-16, 5.750408897959578548E-10 ) ) ;
#431=CARTESIAN_POINT ( 'NONE',  ( 3.562500000000000444, -3.820994442221351629E-18, 2.975000000000000977 ) ) ;
#434=CIRCLE ( 'NONE', #4088, 0.3625000012227142521 ) ;
#437=CARTESIAN_POINT ( 'NONE',  ( -3.562500000000000444, 0.000000000000000000, 2.612499999999998934 ) ) ;
#438=AXIS2_PLACEMENT_3D ( 'NONE', #2910, #5407, #4176 ) ;
#455=CARTESIAN_POINT ( 'NONE',  ( 2.513411990276540831, 1.000000000000000222, -2.949302488239232023 ) ) ;
#459=CARTESIAN_POINT ( 'NONE',  ( -3.762484563843162100, 1.281112611882646579, 4.607714677951853639E-16 ) ) ;
#462=DIRECTION ( 'NONE',  ( -0.000000000000000000, -1.000000000000000000, -0.000000000000000000 ) ) ;
#463=AXIS2_PLACEMENT_3D ( 'NONE', #727, #2610, #4482 ) ;
#468=( BOUNDED_CURVE ( )  B_SPLINE_CURVE ( 3, ( #2510, #4305, #4339, #1282 ),
 .UNSPECIFIED., .F., .F. ) 
 B_SPLINE_CURVE_WITH_KNOTS ( ( 4, 4 ),
 ( 0.000000000000000000, 0.03896959995064044890 ),
 .UNSPECIFIED. ) 
 CURVE ( )  GEOMETRIC_REPRESENTATION_ITEM ( )  RATIONAL_B_SPLINE_CURVE ( ( 0.5120000962196032956, 0.5230192003547537993, 0.5416270346375180456, 0.5678235990678961453 ) ) 
 REPRESENTATION_ITEM ( '' )  );
#474=ORIENTED_EDGE ( 'NONE', *, *, #817, .T. ) ;
#479=EDGE_CURVE ( 'NONE', #1080, #2357, #5711, .T. ) ;
#481=CARTESIAN_POINT ( 'NONE',  ( -2.861675873811764248, 1.000000000000000222, -2.612744953730403719 ) ) ;
#485=ORIENTED_EDGE ( 'NONE', *, *, #3629, .F. ) ;
#495=CARTESIAN_POINT ( 'NONE',  ( 3.687499987877262519, 1.365923996832131609E-16, 3.874999999790589289 ) ) ;
#496=DIRECTION ( 'NONE',  ( 0.000000000000000000, -1.000000000000000000, 0.000000000000000000 ) ) ;
#517=EDGE_LOOP ( 'NONE', ( #6881, #3552, #6154, #4869 ) ) ;
#522=CARTESIAN_POINT ( 'NONE',  ( -2.875000000000000888, 0.000000000000000000, -3.337500001222715174 ) ) ;
#527=CARTESIAN_POINT ( 'NONE',  ( -2.861675873811764248, 1.000000000000000222, -2.612744953730403719 ) ) ;
#535=ORIENTED_EDGE ( 'NONE', *, *, #479, .T. ) ;
#537=LINE ( 'NONE', #4804, #181 ) ;
#543=DIRECTION ( 'NONE',  ( -0.000000000000000000, 1.000000000000000000, -0.000000000000000000 ) ) ;
#554=ORIENTED_EDGE ( 'NONE', *, *, #1085, .F. ) ;
#562=EDGE_CURVE ( 'NONE', #6048, #2229, #7985, .T. ) ;
#563=CARTESIAN_POINT ( 'NONE',  ( 2.861675873811764248, 1.000000000000000222, -2.612744953730403719 ) ) ;
#566=ORIENTED_EDGE ( 'NONE', *, *, #3549, .F. ) ;
#583=CARTESIAN_POINT ( 'NONE',  ( 3.562500000000000444, 1.000000000000000222, 2.975000000000000977 ) ) ;
#584=VERTEX_POINT ( 'NONE', #7193 ) ;
#589=EDGE_CURVE ( 'NONE', #5981, #8092, #4393, .T. ) ;
#591=AXIS2_PLACEMENT_3D ( 'NONE', #1766, #3689, #7532 ) ;
#601=EDGE_CURVE ( 'NONE', #3043, #3479, #4261, .T. ) ;
#605=VERTEX_POINT ( 'NONE', #3537 ) ;
#611=AXIS2_PLACEMENT_3D ( 'NONE', #6702, #6046, #6592 ) ;
#615=VERTEX_POINT ( 'NONE', #2960 ) ;
#628=ORIENTED_EDGE ( 'NONE', *, *, #4363, .T. ) ;
#629=ORIENTED_EDGE ( 'NONE', *, *, #1150, .T. ) ;
#632=EDGE_CURVE ( 'NONE', #2164, #7244, #5794, .T. ) ;
#638=CARTESIAN_POINT ( 'NONE',  ( -1.172489671586611548, 1.365923996832131609E-16, -3.693357951819908891 ) ) ;
#641=CYLINDRICAL_SURFACE ( 'NONE', #6649, 5.349138356872925826 ) ;
#645=ORIENTED_EDGE ( 'NONE', *, *, #6517, .F. ) ;
#652=PLANE ( 'NONE',  #1485 ) ;
#659=ADVANCED_BREP_SHAPE_REPRESENTATION ( '', ( #4597, #7272 ), #3062 ) ;
#661=CARTESIAN_POINT ( 'NONE',  ( -2.875000000000000888, -3.820994292482255198E-18, -2.975000000000000977 ) ) ;
#675=EDGE_CURVE ( 'NONE', #2688, #7591, #5453, .T. ) ;
#679=LINE ( 'NONE', #3142, #2459 ) ;
#688=EDGE_CURVE ( 'NONE', #7723, #4873, #1653, .T. ) ;
#690=CARTESIAN_POINT ( 'NONE',  ( 3.362500000000000711, 1.750000000000000444, 0.000000000000000000 ) ) ;
#693=CYLINDRICAL_SURFACE ( 'NONE', #8106, 0.3625000000000019318 ) ;
#696=ORIENTED_EDGE ( 'NONE', *, *, #6452, .T. ) ;
#702=VECTOR ( 'NONE', #8171, 39.37007874015748143 ) ;
#714=DIRECTION ( 'NONE',  ( -0.000000000000000000, -1.000000000000000000, -0.000000000000000000 ) ) ;
#715=ORIENTED_EDGE ( 'NONE', *, *, #4776, .F. ) ;
#719=AXIS2_PLACEMENT_3D ( 'NONE', #901, #7260, #5863 ) ;
#727=CARTESIAN_POINT ( 'NONE',  ( -8.751021560936518753E-10, 1.000000000000000222, 5.750408897959578548E-10 ) ) ;
#728=AXIS2_PLACEMENT_3D ( 'NONE', #845, #392, #7206 ) ;
#729=DIRECTION ( 'NONE',  ( 0.000000000000000000, -0.000000000000000000, 1.000000000000000000 ) ) ;
#743=EDGE_CURVE ( 'NONE', #2413, #2164, #1918, .T. ) ;
#745=CARTESIAN_POINT ( 'NONE',  ( -3.791570908345035740, 1.000000000000000222, 0.7997593681799636256 ) ) ;
#750=VERTEX_POINT ( 'NONE', #6005 ) ;
#753=AXIS2_PLACEMENT_3D ( 'NONE', #2039, #4412, #5103 ) ;
#766=DIRECTION ( 'NONE',  ( 0.000000000000000000, 0.000000000000000000, -1.000000000000000000 ) ) ;
#770=ORIENTED_EDGE ( 'NONE', *, *, #2486, .F. ) ;
#771=DIRECTION ( 'NONE',  ( 0.000000000000000000, 0.000000000000000000, -1.000000000000000000 ) ) ;
#776=EDGE_CURVE ( 'NONE', #7088, #2216, #3505, .T. ) ;
#784=EDGE_CURVE ( 'NONE', #7591, #8139, #5850, .T. ) ;
#788=CARTESIAN_POINT ( 'NONE',  ( -3.687499989627467389, 1.365923996832131609E-16, 3.874999999790589289 ) ) ;
#797=FACE_OUTER_BOUND ( 'NONE', #1020, .T. ) ;
#809=ORIENTED_EDGE ( 'NONE', *, *, #688, .F. ) ;
#817=EDGE_CURVE ( 'NONE', #1533, #750, #7991, .T. ) ;
#819=DIRECTION ( 'NONE',  ( 0.000000000000000000, 1.000000000000000000, 0.000000000000000000 ) ) ;
#841=FACE_OUTER_BOUND ( 'NONE', #3872, .T. ) ;
#845=CARTESIAN_POINT ( 'NONE',  ( 2.875000000000000888, 0.000000000000000000, -2.975000000000000977 ) ) ;
#854=ORIENTED_EDGE ( 'NONE', *, *, #4776, .T. ) ;
#855=DIRECTION ( 'NONE',  ( 0.000000000000000000, 0.000000000000000000, -1.000000000000000000 ) ) ;
#869=AXIS2_PLACEMENT_3D ( 'NONE', #7283, #1655, #7234 ) ;
#871=DIRECTION ( 'NONE',  ( -0.9917930140139561423, 0.000000000000000000, 0.1278538906451907597 ) ) ;
#874=CARTESIAN_POINT ( 'NONE',  ( -3.791570908345035740, 1.365923996832131609E-16, 0.7997593681799639587 ) ) ;
#878=EDGE_CURVE ( 'NONE', #6680, #5163, #6113, .T. ) ;
#885=CARTESIAN_POINT ( 'NONE',  ( 3.651126734928074491, 1.365923996832131609E-16, -1.298036420927625167 ) ) ;
#898=CARTESIAN_POINT ( 'NONE',  ( 1.462953684461641091, 1.365923996832131609E-16, 3.588229578933126440 ) ) ;
#901=CARTESIAN_POINT ( 'NONE',  ( -8.751021560936518753E-10, 1.000000000000000222, 5.750408897959578548E-10 ) ) ;
#912=EDGE_LOOP ( 'NONE', ( #8131, #2717 ) ) ;
#913=FACE_OUTER_BOUND ( 'NONE', #7401, .T. ) ;
#916=CARTESIAN_POINT ( 'NONE',  ( -3.224046040006844027, 0.9999999999998147038, -2.215849741854215793 ) ) ;
#917=ORIENTED_EDGE ( 'NONE', *, *, #5026, .F. ) ;
#922=DIRECTION ( 'NONE',  ( -0.000000000000000000, 1.000000000000000000, -0.000000000000000000 ) ) ;
#926=EDGE_CURVE ( 'NONE', #2164, #605, #7448, .T. ) ;
#930=DIRECTION ( 'NONE',  ( 0.000000000000000000, -1.000000000000000000, 0.000000000000000000 ) ) ;
#933=ORIENTED_EDGE ( 'NONE', *, *, #6659, .T. ) ;
#934=FACE_OUTER_BOUND ( 'NONE', #5620, .T. ) ;
#936=EDGE_LOOP ( 'NONE', ( #5279, #1727, #4391, #1423 ) ) ;
#953=CARTESIAN_POINT ( 'NONE',  ( -3.796513189164428148, 1.000000000000000666, -2.946478859991636057 ) ) ;
#969=CARTESIAN_POINT ( 'NONE',  ( -8.751021560936518753E-10, 1.000000000000000222, 5.750408897959578548E-10 ) ) ;
#972=DIRECTION ( 'NONE',  ( -0.000000000000000000, 1.000000000000000000, -0.000000000000000000 ) ) ;
#987=VERTEX_POINT ( 'NONE', #4240 ) ;
#989=CARTESIAN_POINT ( 'NONE',  ( 3.651126735575231042, 1.000000000000000222, -1.298036422080803165 ) ) ;
#999=CARTESIAN_POINT ( 'NONE',  ( -3.362500000000001155, 1.750000000000000444, 4.117874862132976456E-16 ) ) ;
#1006=DIRECTION ( 'NONE',  ( -0.000000000000000000, 1.000000000000000000, -0.000000000000000000 ) ) ;
#1014=AXIS2_PLACEMENT_3D ( 'NONE', #1065, #3557, #4200 ) ;
#1016=CARTESIAN_POINT ( 'NONE',  ( -3.796513189164426816, 1.365923996832131609E-16, -2.946478859991635169 ) ) ;
#1020=EDGE_LOOP ( 'NONE', ( #1948, #5905, #4612, #7659 ) ) ;
#1021=LINE ( 'NONE', #437, #3102 ) ;
#1039=EDGE_LOOP ( 'NONE', ( #933, #4900, #258, #5263, #375, #6338, #2581, #3852 ) ) ;
#1043=DIRECTION ( 'NONE',  ( 0.000000000000000000, 0.000000000000000000, -1.000000000000000000 ) ) ;
#1065=CARTESIAN_POINT ( 'NONE',  ( -8.751021560936518753E-10, 1.000000000000000222, 5.750408897959578548E-10 ) ) ;
#1067=ORIENTED_EDGE ( 'NONE', *, *, #6553, .F. ) ;
#1075=ORIENTED_EDGE ( 'NONE', *, *, #4838, .F. ) ;
#1080=VERTEX_POINT ( 'NONE', #1908 ) ;
#1085=EDGE_CURVE ( 'NONE', #2688, #5456, #679, .T. ) ;
#1088=DIRECTION ( 'NONE',  ( 0.08785522361217637521, 0.000000000000000000, -0.9961332539796342589 ) ) ;
#1092=ADVANCED_FACE ( 'NONE', ( #8121 ), #53, .F. ) ;
#1094=CARTESIAN_POINT ( 'NONE',  ( -1.172489671586610660, 1.365923996832131609E-16, -3.693357951819909779 ) ) ;
#1096=ORIENTED_EDGE ( 'NONE', *, *, #3735, .F. ) ;
#1098=VECTOR ( 'NONE', #4453, 39.37007874015748143 ) ;
#1110=AXIS2_PLACEMENT_3D ( 'NONE', #6443, #819, #157 ) ;
#1128=AXIS2_PLACEMENT_3D ( 'NONE', #1669, #6786, #7300 ) ;
#1149=CARTESIAN_POINT ( 'NONE',  ( -2.513411990276539942, 1.000000000000000444, -2.949302488239234243 ) ) ;
#1150=EDGE_CURVE ( 'NONE', #5154, #2549, #2289, .T. ) ;
#1153=DIRECTION ( 'NONE',  ( -0.000000000000000000, -1.000000000000000000, -0.000000000000000000 ) ) ;
#1161=CARTESIAN_POINT ( 'NONE',  ( 3.651126734928074491, 1.000000000000000888, -1.298036420927625167 ) ) ;
#1163=EDGE_CURVE ( 'NONE', #6966, #4981, #5316, .T. ) ;
#1164=PRODUCT_DEFINITION_FORMATION_WITH_SPECIFIED_SOURCE ( 'ANY', '', #1774, .NOT_KNOWN. ) ;
#1169=CYLINDRICAL_SURFACE ( 'NONE', #5836, 0.3625000000000019318 ) ;
#1173=EDGE_CURVE ( 'NONE', #1938, #5163, #4437, .T. ) ;
#1174=EDGE_LOOP ( 'NONE', ( #86, #184, #3850, #2849 ) ) ;
#1177=ORIENTED_EDGE ( 'NONE', *, *, #878, .F. ) ;
#1187=CARTESIAN_POINT ( 'NONE',  ( 1.172489670925565663, 1.365923996832131609E-16, -3.693357951474146361 ) ) ;
#1188=DIRECTION ( 'NONE',  ( 0.000000000000000000, 0.000000000000000000, -1.000000000000000000 ) ) ;
#1191=DIRECTION ( 'NONE',  ( -0.000000000000000000, -1.000000000000000000, -0.000000000000000000 ) ) ;
#1195=LINE ( 'NONE', #6075, #4099 ) ;
#1210=EDGE_CURVE ( 'NONE', #1295, #2112, #2323, .T. ) ;
#1218=CIRCLE ( 'NONE', #6193, 0.3625000000000019318 ) ;
#1223=ORIENTED_EDGE ( 'NONE', *, *, #6059, .F. ) ;
#1226=ADVANCED_FACE ( 'NONE', ( #913 ), #213, .F. ) ;
#1229=ORIENTED_EDGE ( 'NONE', *, *, #4588, .T. ) ;
#1230=CIRCLE ( 'NONE', #5669, 2.845000000000001528 ) ;
#1235=AXIS2_PLACEMENT_3D ( 'NONE', #5040, #7619, #7581 ) ;
#1253=DIRECTION ( 'NONE',  ( 0.9925485533740562305, 0.000000000000000000, 0.1218497812680350845 ) ) ;
#1261=ORIENTED_EDGE ( 'NONE', *, *, #7159, .F. ) ;
#1272=DIRECTION ( 'NONE',  ( -0.000000000000000000, 1.000000000000000000, -0.000000000000000000 ) ) ;
#1282=CARTESIAN_POINT ( 'NONE',  ( -2.513411990276539942, 1.000000000000000444, -2.949302488239234243 ) ) ;
#1284=DIRECTION ( 'NONE',  ( 9.769962616696322535E-15, 0.000000000000000000, 1.000000000000000000 ) ) ;
#1289=CARTESIAN_POINT ( 'NONE',  ( -3.651126736170069886, 1.365923996832131609E-16, -1.298036422357116138 ) ) ;
#1294=FACE_OUTER_BOUND ( 'NONE', #4962, .T. ) ;
#1295=VERTEX_POINT ( 'NONE', #953 ) ;
#1302=CARTESIAN_POINT ( 'NONE',  ( -2.875000000000000888, 1.000000000000000222, -2.975000000000000977 ) ) ;
#1304=LINE ( 'NONE', #4534, #5856 ) ;
#1306=CARTESIAN_POINT ( 'NONE',  ( 1.462953684860233805, 1.000000000000000666, 3.588229579187919960 ) ) ;
#1332=ADVANCED_FACE ( 'NONE', ( #4797 ), #7774, .T. ) ;
#1333=FACE_BOUND ( 'NONE', #4286, .T. ) ;
#1342=CARTESIAN_POINT ( 'NONE',  ( 2.875000000000000888, 0.000000000000000000, -3.337500001222715174 ) ) ;
#1352=ORIENTED_EDGE ( 'NONE', *, *, #1173, .T. ) ;
#1368=DESIGN_CONTEXT ( 'detailed design', #4603, 'design' ) ;
#1381=EDGE_CURVE ( 'NONE', #4517, #3043, #6117, .T. ) ;
#1389=VECTOR ( 'NONE', #3934, 39.37007874015748143 ) ;
#1390=EDGE_LOOP ( 'NONE', ( #3054, #7873, #5510, #5186 ) ) ;
#1397=ORIENTED_EDGE ( 'NONE', *, *, #1873, .F. ) ;
#1400=CARTESIAN_POINT ( 'NONE',  ( 3.484120143574221651E-16, 1.750000000000000444, 2.845000000000001528 ) ) ;
#1410=EDGE_CURVE ( 'NONE', #1993, #3049, #5415, .T. ) ;
#1421=CYLINDRICAL_SURFACE ( 'NONE', #2304, 0.3625000000000019318 ) ;
#1423=ORIENTED_EDGE ( 'NONE', *, *, #4838, .T. ) ;
#1430=CARTESIAN_POINT ( 'NONE',  ( 1.172489670925564997, 1.365923996832131609E-16, -3.693357951474146805 ) ) ;
#1437=EDGE_LOOP ( 'NONE', ( #4155, #4340, #3099, #7213 ) ) ;
#1442=VERTEX_POINT ( 'NONE', #2474 ) ;
#1453=CARTESIAN_POINT ( 'NONE',  ( -3.362500000000001155, 1.750000000000000444, 4.117874862132976456E-16 ) ) ;
#1457=CARTESIAN_POINT ( 'NONE',  ( -3.791570908345035740, 1.000000000000000222, 0.7997593681799639587 ) ) ;
#1460=ORIENTED_EDGE ( 'NONE', *, *, #4983, .F. ) ;
#1467=( BOUNDED_CURVE ( )  B_SPLINE_CURVE ( 3, ( #1453, #3930, #1654, #4177 ),
 .UNSPECIFIED., .F., .F. ) 
 B_SPLINE_CURVE_WITH_KNOTS ( ( 4, 4 ),
 ( 0.000000000000000000, 0.2669680800879516980 ),
 .UNSPECIFIED. ) 
 CURVE ( )  GEOMETRIC_REPRESENTATION_ITEM ( )  RATIONAL_B_SPLINE_CURVE ( ( 1.000000000000000000, 0.3333333333333334259, 0.3333333333333334259, 1.000000000000000000 ) ) 
 REPRESENTATION_ITEM ( '' )  );
#1468=EDGE_CURVE ( 'NONE', #1711, #295, #4959, .T. ) ;
#1469=VERTEX_POINT ( 'NONE', #5575 ) ;
#1472=ORIENTED_EDGE ( 'NONE', *, *, #1085, .T. ) ;
#1480=LINE ( 'NONE', #5320, #3329 ) ;
#1485=AXIS2_PLACEMENT_3D ( 'NONE', #690, #4950, #1839 ) ;
#1488=AXIS2_PLACEMENT_3D ( 'NONE', #1760, #4790, #7955 ) ;
#1489=EDGE_CURVE ( 'NONE', #5456, #2413, #468, .T. ) ;
#1503=DIRECTION ( 'NONE',  ( 0.000000000000000000, 0.000000000000000000, 1.000000000000000000 ) ) ;
#1506=PLANE ( 'NONE',  #6080 ) ;
#1510=DIRECTION ( 'NONE',  ( -0.000000000000000000, -1.000000000000000000, -0.000000000000000000 ) ) ;
#1512=VECTOR ( 'NONE', #5979, 39.37007874015748143 ) ;
#1515=DIRECTION ( 'NONE',  ( 0.1218497814115311745, 0.000000000000000000, 0.9925485533564400997 ) ) ;
#1529=CARTESIAN_POINT ( 'NONE',  ( -2.875000000000000888, 0.000000000000000000, -2.975000000000000977 ) ) ;
#1533=VERTEX_POINT ( 'NONE', #5696 ) ;
#1552=CYLINDRICAL_SURFACE ( 'NONE', #4481, 0.3625000000000019318 ) ;
#1557=CARTESIAN_POINT ( 'NONE',  ( -3.796513189164424151, 1.365923996832131609E-16, -2.946478859991638277 ) ) ;
#1560=DIRECTION ( 'NONE',  ( 0.000000000000000000, 0.000000000000000000, -1.000000000000000000 ) ) ;
#1562=ORIENTED_EDGE ( 'NONE', *, *, #3394, .F. ) ;
#1566=DIRECTION ( 'NONE',  ( 0.000000000000000000, 0.000000000000000000, -1.000000000000000000 ) ) ;
#1575=CARTESIAN_POINT ( 'NONE',  ( -3.484361157709182422, 0.9999999999998147038, -1.767115912624255047 ) ) ;
#1609=CARTESIAN_POINT ( 'NONE',  ( -3.762484563843160768, 1.281112611882646579, 7.524969127686321535 ) ) ;
#1623=LINE ( 'NONE', #5500, #3959 ) ;
#1635=DIRECTION ( 'NONE',  ( 0.000000000000000000, 1.000000000000000000, 0.000000000000000000 ) ) ;
#1636=ORIENTED_EDGE ( 'NONE', *, *, #562, .T. ) ;
#1640=ORIENTED_EDGE ( 'NONE', *, *, #3371, .F. ) ;
#1653=CIRCLE ( 'NONE', #4522, 4.805751768934915624 ) ;
#1654=CARTESIAN_POINT ( 'NONE',  ( 3.362499999999998934, 1.750000000000000000, -6.725000000000002309 ) ) ;
#1655=DIRECTION ( 'NONE',  ( -0.000000000000000000, -1.000000000000000000, -0.000000000000000000 ) ) ;
#1669=CARTESIAN_POINT ( 'NONE',  ( -8.751021560936518753E-10, 1.365923996832131609E-16, 5.750408897959578548E-10 ) ) ;
#1676=DIRECTION ( 'NONE',  ( -0.000000000000000000, 1.000000000000000000, -0.000000000000000000 ) ) ;
#1680=DIRECTION ( 'NONE',  ( -0.000000000000000000, -1.000000000000000000, -0.000000000000000000 ) ) ;
#1692=CARTESIAN_POINT ( 'NONE',  ( 3.762484563843161212, 1.281112611882646579, -9.215429355903707278E-16 ) ) ;
#1693=CARTESIAN_POINT ( 'NONE',  ( 2.875000000000000888, 1.000000000000000222, -2.975000000000000977 ) ) ;
#1700=DIRECTION ( 'NONE',  ( 0.08785522361217638909, -0.000000000000000000, -0.9961332539796342589 ) ) ;
#1701=VERTEX_POINT ( 'NONE', #7134 ) ;
#1708=ORIENTED_EDGE ( 'NONE', *, *, #7050, .F. ) ;
#1711=VERTEX_POINT ( 'NONE', #1400 ) ;
#1712=CARTESIAN_POINT ( 'NONE',  ( -2.875000000000000888, 0.000000000000000000, -2.975000000000000977 ) ) ;
#1719=DIRECTION ( 'NONE',  ( 0.000000000000000000, 0.000000000000000000, 1.000000000000000000 ) ) ;
#1727=ORIENTED_EDGE ( 'NONE', *, *, #5433, .T. ) ;
#1728=DIRECTION ( 'NONE',  ( 0.000000000000000000, 0.000000000000000000, -1.000000000000000000 ) ) ;
#1738=DIRECTION ( 'NONE',  ( 0.000000000000000000, -1.000000000000000000, 0.000000000000000000 ) ) ;
#1744=CARTESIAN_POINT ( 'NONE',  ( 3.791570906296184873, 1.365923996832131609E-16, 0.7997593695958172821 ) ) ;
#1751=AXIS2_PLACEMENT_3D ( 'NONE', #7281, #2758, #380 ) ;
#1753=CYLINDRICAL_SURFACE ( 'NONE', #4379, 3.874999999025058539 ) ;
#1760=CARTESIAN_POINT ( 'NONE',  ( -2.875000000000000888, 1.000000000000000222, -2.975000000000000977 ) ) ;
#1762=AXIS2_PLACEMENT_3D ( 'NONE', #4335, #4837, #1188 ) ;
#1763=ORIENTED_EDGE ( 'NONE', *, *, #562, .F. ) ;
#1766=CARTESIAN_POINT ( 'NONE',  ( -8.751021560936518753E-10, 1.365923996832131609E-16, 5.750408897959578548E-10 ) ) ;
#1770=CARTESIAN_POINT ( 'NONE',  ( -3.874999999933440797, 1.000000000000000222, -5.476399496138180442E-16 ) ) ;
#1774=PRODUCT ( 'bench vise-', 'bench vise-', '', ( #6614 ) ) ;
#1775=EDGE_LOOP ( 'NONE', ( #6851, #3554, #2147, #5382 ) ) ;
#1781=ORIENTED_EDGE ( 'NONE', *, *, #7046, .T. ) ;
#1791=DIRECTION ( 'NONE',  ( 0.000000000000000000, -1.000000000000000000, 0.000000000000000000 ) ) ;
#1794=AXIS2_PLACEMENT_3D ( 'NONE', #431, #2925, #3636 ) ;
#1809=CARTESIAN_POINT ( 'NONE',  ( 4.470366332363715500, 1.365923996832131609E-16, 2.937534001674281914 ) ) ;
#1818=ORIENTED_EDGE ( 'NONE', *, *, #5751, .F. ) ;
#1829=PLANE ( 'NONE',  #5952 ) ;
#1834=ADVANCED_FACE ( 'NONE', ( #7491 ), #1921, .T. ) ;
#1835=LINE ( 'NONE', #522, #5559 ) ;
#1839=DIRECTION ( 'NONE',  ( 0.000000000000000000, -0.000000000000000000, 1.000000000000000000 ) ) ;
#1840=VERTEX_POINT ( 'NONE', #495 ) ;
#1852=EDGE_LOOP ( 'NONE', ( #5633, #153, #645, #2099, #2845, #4446, #5523, #3750, #6863, #1861, #5608, #5761 ) ) ;
#1861=ORIENTED_EDGE ( 'NONE', *, *, #1873, .T. ) ;
#1873=EDGE_CURVE ( 'NONE', #5810, #3375, #3238, .T. ) ;
#1892=ORIENTED_EDGE ( 'NONE', *, *, #2792, .T. ) ;
#1903=DIRECTION ( 'NONE',  ( 0.000000000000000000, -1.000000000000000000, 0.000000000000000000 ) ) ;
#1908=CARTESIAN_POINT ( 'NONE',  ( -3.562500000000000444, 1.000000000000000222, 3.337500000000003020 ) ) ;
#1918=CIRCLE ( 'NONE', #611, 0.3625000012227142521 ) ;
#1921=CYLINDRICAL_SURFACE ( 'NONE', #2572, 3.874999999025058095 ) ;
#1938=VERTEX_POINT ( 'NONE', #1306 ) ;
#1948=ORIENTED_EDGE ( 'NONE', *, *, #3536, .F. ) ;
#1954=CARTESIAN_POINT ( 'NONE',  ( -3.687499989627468722, 1.365923996832131609E-16, 3.874999999790587513 ) ) ;
#1968=ORIENTED_EDGE ( 'NONE', *, *, #8016, .F. ) ;
#1979=ADVANCED_FACE ( 'NONE', ( #934 ), #6566, .F. ) ;
#1986=DIRECTION ( 'NONE',  ( 0.000000000000000000, -0.000000000000000000, 1.000000000000000000 ) ) ;
#1993=VERTEX_POINT ( 'NONE', #6013 ) ;
#2010=LENGTH_MEASURE_WITH_UNIT ( LENGTH_MEASURE( 0.02539999999999999897 ), #7657 );
#2021=AXIS2_PLACEMENT_3D ( 'NONE', #5827, #4506, #5201 ) ;
#2030=FACE_BOUND ( 'NONE', #3861, .T. ) ;
#2039=CARTESIAN_POINT ( 'NONE',  ( -8.751021560936518753E-10, 1.365923996832131609E-16, 5.750408897959578548E-10 ) ) ;
#2041=EDGE_LOOP ( 'NONE', ( #4332, #1397, #7612, #6170, #4087, #7748, #2793, #6161 ) ) ;
#2044=EDGE_CURVE ( 'NONE', #615, #1469, #1021, .T. ) ;
#2049=ORIENTED_EDGE ( 'NONE', *, *, #3536, .T. ) ;
#2072=LINE ( 'NONE', #1457, #6719 ) ;
#2076=ORIENTED_EDGE ( 'NONE', *, *, #5957, .F. ) ;
#2088=ORIENTED_EDGE ( 'NONE', *, *, #4953, .T. ) ;
#2099=ORIENTED_EDGE ( 'NONE', *, *, #1410, .T. ) ;
#2112=VERTEX_POINT ( 'NONE', #5552 ) ;
#2116=CARTESIAN_POINT ( 'NONE',  ( 3.583510604133040900, 1.543025754838327046, -8.777069582124253846E-16 ) ) ;
#2124=DIRECTION ( 'NONE',  ( -0.000000000000000000, -1.000000000000000000, -0.000000000000000000 ) ) ;
#2132=FACE_OUTER_BOUND ( 'NONE', #7370, .T. ) ;
#2141=CIRCLE ( 'NONE', #438, 3.874999999025058539 ) ;
#2143=ADVANCED_FACE ( 'NONE', ( #8119 ), #8160, .F. ) ;
#2147=ORIENTED_EDGE ( 'NONE', *, *, #3549, .T. ) ;
#2148=AXIS2_PLACEMENT_3D ( 'NONE', #7530, #147, #66 ) ;
#2154=DIRECTION ( 'NONE',  ( -0.000000000000000000, 1.000000000000000000, -0.000000000000000000 ) ) ;
#2159=CARTESIAN_POINT ( 'NONE',  ( -8.751021560936518753E-10, 1.000000000000000222, 5.750408897959578548E-10 ) ) ;
#2164=VERTEX_POINT ( 'NONE', #481 ) ;
#2170=ORIENTED_EDGE ( 'NONE', *, *, #6517, .T. ) ;
#2172=DIRECTION ( 'NONE',  ( 0.000000000000000000, -1.000000000000000000, 0.000000000000000000 ) ) ;
#2176=AXIS2_PLACEMENT_3D ( 'NONE', #7972, #2310, #5328 ) ;
#2182=LINE ( 'NONE', #415, #7550 ) ;
#2186=VERTEX_POINT ( 'NONE', #4978 ) ;
#2188=CIRCLE ( 'NONE', #5526, 3.874999999025058095 ) ;
#2194=CIRCLE ( 'NONE', #753, 3.874999999025058539 ) ;
#2200=DIRECTION ( 'NONE',  ( 0.000000000000000000, 0.000000000000000000, 1.000000000000000000 ) ) ;
#2212=EDGE_LOOP ( 'NONE', ( #2347, #1640, #5202, #2088 ) ) ;
#2214=PLANE ( 'NONE',  #48 ) ;
#2216=VERTEX_POINT ( 'NONE', #4287 ) ;
#2221=CARTESIAN_POINT ( 'NONE',  ( 3.875000000000001776, 1.000000000000000222, 0.000000000000000000 ) ) ;
#2229=VERTEX_POINT ( 'NONE', #5508 ) ;
#2240=ORIENTED_EDGE ( 'NONE', *, *, #6413, .F. ) ;
#2242=EDGE_LOOP ( 'NONE', ( #3589, #2076 ) ) ;
#2244=EDGE_LOOP ( 'NONE', ( #6043, #5590, #111, #1261, #4964, #3550, #2524, #270, #6251 ) ) ;
#2262=LINE ( 'NONE', #1161, #4085 ) ;
#2263=ORIENTED_EDGE ( 'NONE', *, *, #4730, .T. ) ;
#2264=AXIS2_PLACEMENT_3D ( 'NONE', #178, #7719, #1503 ) ;
#2274=DIRECTION ( 'NONE',  ( -0.08785522444269551479, 0.000000000000000000, -0.9961332539063855185 ) ) ;
#2277=ADVANCED_FACE ( 'NONE', ( #6254 ), #641, .T. ) ;
#2289=LINE ( 'NONE', #4787, #5720 ) ;
#2296=CARTESIAN_POINT ( 'NONE',  ( 3.562500000000000444, 1.000000000000000222, 2.975000000000000977 ) ) ;
#2300=CARTESIAN_POINT ( 'NONE',  ( 3.875000000000001776, 1.000000000000000222, 7.750000000000002665 ) ) ;
#2303=CARTESIAN_POINT ( 'NONE',  ( -3.583510604133042232, 1.543025754838326824, -7.167021208266081800 ) ) ;
#2304=AXIS2_PLACEMENT_3D ( 'NONE', #6993, #5795, #3258 ) ;
#2310=DIRECTION ( 'NONE',  ( -0.000000000000000000, -1.000000000000000000, -0.000000000000000000 ) ) ;
#2323=CIRCLE ( 'NONE', #6242, 4.805751768934915624 ) ;
#2325=CARTESIAN_POINT ( 'NONE',  ( 3.562500000000000444, -3.820994442221351629E-18, 2.612499999999998934 ) ) ;
#2332=ORIENTED_EDGE ( 'NONE', *, *, #6452, .F. ) ;
#2340=DIRECTION ( 'NONE',  ( 0.000000000000000000, 0.000000000000000000, -1.000000000000000000 ) ) ;
#2347=ORIENTED_EDGE ( 'NONE', *, *, #1150, .F. ) ;
#2349=DIRECTION ( 'NONE',  ( -0.000000000000000000, -1.000000000000000000, -0.000000000000000000 ) ) ;
#2357=VERTEX_POINT ( 'NONE', #3488 ) ;
#2359=CARTESIAN_POINT ( 'NONE',  ( -3.687499989627468278, 1.000000000000000666, 3.874999999790589733 ) ) ;
#2364=FACE_OUTER_BOUND ( 'NONE', #8053, .T. ) ;
#2388=CARTESIAN_POINT ( 'NONE',  ( -3.875000000000002220, 1.000000000000000222, 4.745506346695996852E-16 ) ) ;
#2401=ORIENTED_EDGE ( 'NONE', *, *, #6398, .F. ) ;
#2409=CIRCLE ( 'NONE', #3954, 0.3625000000000019318 ) ;
#2413=VERTEX_POINT ( 'NONE', #4740 ) ;
#2423=CARTESIAN_POINT ( 'NONE',  ( 3.791570907149167446, 1.000000000000000222, 0.7997593697006841751 ) ) ;
#2428=DIRECTION ( 'NONE',  ( -0.3026345437601030697, -0.000000000000000000, -0.9531066744720204653 ) ) ;
#2432=CIRCLE ( 'NONE', #591, 5.349138356872925826 ) ;
#2438=VECTOR ( 'NONE', #5967, 39.37007874015748143 ) ;
#2442=ORIENTED_EDGE ( 'NONE', *, *, #8079, .F. ) ;
#2459=VECTOR ( 'NONE', #5675, 39.37007874015748143 ) ;
#2474=CARTESIAN_POINT ( 'NONE',  ( 4.470366332363715500, 1.365923996832131609E-16, 2.937534001674282358 ) ) ;
#2479=( CONVERSION_BASED_UNIT ( 'INCH', #2010 ) LENGTH_UNIT ( ) NAMED_UNIT ( #5699 ) );
#2486=EDGE_CURVE ( 'NONE', #4681, #2413, #5185, .T. ) ;
#2499=DIRECTION ( 'NONE',  ( 0.000000000000000000, 0.000000000000000000, -1.000000000000000000 ) ) ;
#2510=CARTESIAN_POINT ( 'NONE',  ( -1.172489672300577768, 1.000000000000000888, -3.693357952253316423 ) ) ;
#2512=SHAPE_REPRESENTATION_RELATIONSHIP ( 'NONE' , 'NONE' ,  #4813, #659 ) ;
#2520=ORIENTED_EDGE ( 'NONE', *, *, #776, .T. ) ;
#2524=ORIENTED_EDGE ( 'NONE', *, *, #2537, .F. ) ;
#2528=VERTEX_POINT ( 'NONE', #6261 ) ;
#2532=DIRECTION ( 'NONE',  ( -0.000000000000000000, 1.000000000000000000, -0.000000000000000000 ) ) ;
#2537=EDGE_CURVE ( 'NONE', #1938, #1701, #4008, .T. ) ;
#2544=VERTEX_POINT ( 'NONE', #1430 ) ;
#2549=VERTEX_POINT ( 'NONE', #2735 ) ;
#2552=CIRCLE ( 'NONE', #39, 2.845000000000001528 ) ;
#2560=CARTESIAN_POINT ( 'NONE',  ( 3.224046039892453308, 0.9999999999999642508, -2.215849741979416088 ) ) ;
#2571=CARTESIAN_POINT ( 'NONE',  ( -3.791570908345035740, 1.365923996832131609E-16, 0.7997593681799639587 ) ) ;
#2572=AXIS2_PLACEMENT_3D ( 'NONE', #6920, #1272, #3721 ) ;
#2576=FACE_OUTER_BOUND ( 'NONE', #6657, .T. ) ;
#2581=ORIENTED_EDGE ( 'NONE', *, *, #4250, .T. ) ;
#2587=AXIS2_PLACEMENT_3D ( 'NONE', #4089, #7408, #1728 ) ;
#2594=CARTESIAN_POINT ( 'NONE',  ( 3.791570907149167002, 1.000000000000000222, 0.7997593697006841751 ) ) ;
#2610=DIRECTION ( 'NONE',  ( -0.000000000000000000, 1.000000000000000000, 0.000000000000000000 ) ) ;
#2616=ORIENTED_EDGE ( 'NONE', *, *, #6285, .T. ) ;
#2626=ORIENTED_EDGE ( 'NONE', *, *, #4363, .F. ) ;
#2631=FACE_OUTER_BOUND ( 'NONE', #4895, .T. ) ;
#2644=CARTESIAN_POINT ( 'NONE',  ( 1.462953684461641091, 1.000000000000000888, 3.588229578933126440 ) ) ;
#2663=CARTESIAN_POINT ( 'NONE',  ( -8.751021560936518753E-10, 1.365923996832131609E-16, 3.874999999600099443 ) ) ;
#2681=LINE ( 'NONE', #7666, #4752 ) ;
#2688=VERTEX_POINT ( 'NONE', #1094 ) ;
#2690=AXIS2_PLACEMENT_3D ( 'NONE', #6302, #5635, #7042 ) ;
#2692=LINE ( 'NONE', #5176, #1389 ) ;
#2717=ORIENTED_EDGE ( 'NONE', *, *, #3419, .F. ) ;
#2727=CARTESIAN_POINT ( 'NONE',  ( -1.172489672300577768, 1.000000000000000888, -3.693357952253316423 ) ) ;
#2735=CARTESIAN_POINT ( 'NONE',  ( 3.562500000000000444, -3.820994442221351629E-18, 3.337500000000003020 ) ) ;
#2741=CYLINDRICAL_SURFACE ( 'NONE', #4118, 2.845000000000001528 ) ;
#2745=ORIENTED_EDGE ( 'NONE', *, *, #3499, .F. ) ;
#2746=EDGE_CURVE ( 'NONE', #4873, #2544, #1304, .T. ) ;
#2758=DIRECTION ( 'NONE',  ( -0.000000000000000000, -1.000000000000000000, -0.000000000000000000 ) ) ;
#2775=ORIENTED_EDGE ( 'NONE', *, *, #4013, .F. ) ;
#2776=CARTESIAN_POINT ( 'NONE',  ( 0.000000000000000000, 1.750000000000000444, -2.845000000000001528 ) ) ;
#2778=CARTESIAN_POINT ( 'NONE',  ( -8.751021560936518753E-10, 1.365923996832131609E-16, 5.750408897959578548E-10 ) ) ;
#2792=EDGE_CURVE ( 'NONE', #6928, #987, #2194, .T. ) ;
#2793=ORIENTED_EDGE ( 'NONE', *, *, #7314, .T. ) ;
#2797=AXIS2_PLACEMENT_3D ( 'NONE', #6283, #6780, #3664 ) ;
#2805=ORIENTED_EDGE ( 'NONE', *, *, #6398, .T. ) ;
#2817=CLOSED_SHELL ( 'NONE', ( #5342, #129, #425, #7525, #5808, #6795, #61, #1834, #6900, #6277, #7109, #5405, #1979, #6758, #5478, #6981, #4530, #5582, #5119, #5125, #1226, #2277, #1092, #2978, #6252, #276, #2143, #5839, #1332, #5921, #6605, #6253, #2830, #6323, #7573, #4427, #5737 ) ) ;
#2822=LINE ( 'NONE', #1557, #1512 ) ;
#2823=EDGE_LOOP ( 'NONE', ( #5080, #5628, #4023, #770, #696, #628 ) ) ;
#2827=AXIS2_PLACEMENT_3D ( 'NONE', #1016, #6009, #2274 ) ;
#2830=ADVANCED_FACE ( 'NONE', ( #2576, #7606 ), #12, .T. ) ;
#2836=EDGE_CURVE ( 'NONE', #4873, #6966, #3112, .T. ) ;
#2838=VECTOR ( 'NONE', #1903, 39.37007874015748143 ) ;
#2845=ORIENTED_EDGE ( 'NONE', *, *, #7928, .T. ) ;
#2848=CYLINDRICAL_SURFACE ( 'NONE', #6488, 3.874999999025058539 ) ;
#2849=ORIENTED_EDGE ( 'NONE', *, *, #6036, .T. ) ;
#2856=EDGE_LOOP ( 'NONE', ( #54, #4216, #5574, #2170, #4541 ) ) ;
#2893=DIRECTION ( 'NONE',  ( 0.1278538907425633420, 0.000000000000000000, -0.9917930140014037388 ) ) ;
#2894=CARTESIAN_POINT ( 'NONE',  ( -2.875000000000000888, 1.000000000000000222, -2.975000000000000977 ) ) ;
#2902=CARTESIAN_POINT ( 'NONE',  ( -3.687499989627468722, 1.365923996832131609E-16, 3.874999999790589289 ) ) ;
#2903=CARTESIAN_POINT ( 'NONE',  ( -2.875000000000000888, 1.000000000000000222, -3.337500001222715174 ) ) ;
#2910=CARTESIAN_POINT ( 'NONE',  ( -8.751021560936518753E-10, 1.000000000000000222, 5.750408897959578548E-10 ) ) ;
#2911=VECTOR ( 'NONE', #6386, 39.37007874015748143 ) ;
#2913=CARTESIAN_POINT ( 'NONE',  ( -2.861675873811764248, 1.000000000000000222, -2.612744953730403719 ) ) ;
#2919=DIRECTION ( 'NONE',  ( 0.000000000000000000, -1.000000000000000000, 0.000000000000000000 ) ) ;
#2920=EDGE_CURVE ( 'NONE', #6239, #584, #4100, .T. ) ;
#2925=DIRECTION ( 'NONE',  ( -0.000000000000000000, -1.000000000000000000, -0.000000000000000000 ) ) ;
#2929=AXIS2_PLACEMENT_3D ( 'NONE', #1529, #6067, #4744 ) ;
#2930=CIRCLE ( 'NONE', #2148, 3.874999999025058539 ) ;
#2952=CARTESIAN_POINT ( 'NONE',  ( -2.875000000000000888, -3.820994292482255198E-18, -2.612499998777286780 ) ) ;
#2955=CARTESIAN_POINT ( 'NONE',  ( 3.362499999999999822, 1.750000000000000222, -6.725000000000002309 ) ) ;
#2960=CARTESIAN_POINT ( 'NONE',  ( -3.562500000000000444, 1.000000000000000222, 2.612499999999998934 ) ) ;
#2969=CARTESIAN_POINT ( 'NONE',  ( -3.544128229492827575, 1.000000000000000222, 1.972857802467875565 ) ) ;
#2978=ADVANCED_FACE ( 'NONE', ( #7043 ), #1552, .F. ) ;
#2982=DIRECTION ( 'NONE',  ( -0.000000000000000000, 1.000000000000000000, -0.000000000000000000 ) ) ;
#2993=DIRECTION ( 'NONE',  ( -0.9925485533740562305, -0.000000000000000000, -0.1218497812680350845 ) ) ;
#3006=CARTESIAN_POINT ( 'NONE',  ( 3.362500000000001155, 1.750000000000000222, 6.725000000000002309 ) ) ;
#3010=CARTESIAN_POINT ( 'NONE',  ( -8.751021560936518753E-10, 1.365923996832131609E-16, 5.750408897959578548E-10 ) ) ;
#3016=DIRECTION ( 'NONE',  ( 0.000000000000000000, 0.000000000000000000, -1.000000000000000000 ) ) ;
#3023=EDGE_CURVE ( 'NONE', #6365, #584, #6324, .T. ) ;
#3028=ORIENTED_EDGE ( 'NONE', *, *, #6740, .F. ) ;
#3029=CARTESIAN_POINT ( 'NONE',  ( -4.470366334113919926, 1.000000000000000222, 2.937534001674282358 ) ) ;
#3038=DIRECTION ( 'NONE',  ( 0.000000000000000000, 0.000000000000000000, 1.000000000000000000 ) ) ;
#3042=CARTESIAN_POINT ( 'NONE',  ( 2.861675873811764248, 1.000000000000000222, -2.612744953730403719 ) ) ;
#3043=VERTEX_POINT ( 'NONE', #4798 ) ;
#3045=CARTESIAN_POINT ( 'NONE',  ( -8.751021560936518753E-10, 1.000000000000000222, 5.750408897959578548E-10 ) ) ;
#3049=VERTEX_POINT ( 'NONE', #7326 ) ;
#3054=ORIENTED_EDGE ( 'NONE', *, *, #688, .T. ) ;
#3062=( GEOMETRIC_REPRESENTATION_CONTEXT ( 3 ) GLOBAL_UNCERTAINTY_ASSIGNED_CONTEXT ( ( #7025 ) ) GLOBAL_UNIT_ASSIGNED_CONTEXT ( ( #2479, #6402, #3127 ) ) REPRESENTATION_CONTEXT ( 'NONE', 'WORKASPACE' ) );
#3066=CYLINDRICAL_SURFACE ( 'NONE', #7936, 2.845000000000001528 ) ;
#3078=AXIS2_PLACEMENT_3D ( 'NONE', #3173, #229, #1986 ) ;
#3082=EDGE_CURVE ( 'NONE', #3479, #5810, #434, .T. ) ;
#3086=DIRECTION ( 'NONE',  ( 0.000000000000000000, 0.000000000000000000, 1.000000000000000000 ) ) ;
#3099=ORIENTED_EDGE ( 'NONE', *, *, #6849, .T. ) ;
#3102=VECTOR ( 'NONE', #4154, 39.37007874015748143 ) ;
#3112=LINE ( 'NONE', #5604, #2911 ) ;
#3115=CARTESIAN_POINT ( 'NONE',  ( 1.462953684860233805, 1.000000000000000666, 3.588229579187919960 ) ) ;
#3118=EDGE_CURVE ( 'NONE', #7757, #3161, #5656, .T. ) ;
#3120=CARTESIAN_POINT ( 'NONE',  ( -3.362499999999999822, 1.750000000000000222, 6.725000000000002309 ) ) ;
#3127=( NAMED_UNIT ( * ) SI_UNIT ( $, .STERADIAN. ) SOLID_ANGLE_UNIT ( ) );
#3136=DIRECTION ( 'NONE',  ( 0.000000000000000000, 0.000000000000000000, 1.000000000000000000 ) ) ;
#3142=CARTESIAN_POINT ( 'NONE',  ( -1.172489671586610882, 1.365923996832131609E-16, -3.693357951819908891 ) ) ;
#3152=DIRECTION ( 'NONE',  ( 0.000000000000000000, -1.000000000000000000, 0.000000000000000000 ) ) ;
#3158=FACE_OUTER_BOUND ( 'NONE', #912, .T. ) ;
#3161=VERTEX_POINT ( 'NONE', #3029 ) ;
#3170=ORIENTED_EDGE ( 'NONE', *, *, #2746, .T. ) ;
#3173=CARTESIAN_POINT ( 'NONE',  ( -8.751021560936518753E-10, 1.365923996832131609E-16, 5.750408897959578548E-10 ) ) ;
#3179=CIRCLE ( 'NONE', #2264, 3.874999999025058539 ) ;
#3190=FACE_OUTER_BOUND ( 'NONE', #3634, .T. ) ;
#3194=CARTESIAN_POINT ( 'NONE',  ( -3.562500000000000444, 0.000000000000000000, 2.975000000000000977 ) ) ;
#3198=AXIS2_PLACEMENT_3D ( 'NONE', #107, #5643, #6310 ) ;
#3211=EDGE_CURVE ( 'NONE', #4886, #7925, #3179, .T. ) ;
#3213=ORIENTED_EDGE ( 'NONE', *, *, #3118, .T. ) ;
#3221=VECTOR ( 'NONE', #2919, 39.37007874015748143 ) ;
#3227=LINE ( 'NONE', #1342, #1098 ) ;
#3235=AXIS2_PLACEMENT_3D ( 'NONE', #788, #5783, #871 ) ;
#3238=( BOUNDED_CURVE ( )  B_SPLINE_CURVE ( 3, ( #3874, #6348, #194, #6307 ),
 .UNSPECIFIED., .F., .F. ) 
 B_SPLINE_CURVE_WITH_KNOTS ( ( 4, 4 ),
 ( 0.000000000000000000, 0.03896959999066340607 ),
 .UNSPECIFIED. ) 
 CURVE ( )  GEOMETRIC_REPRESENTATION_ITEM ( )  RATIONAL_B_SPLINE_CURVE ( ( 0.5678235990678962564, 0.5416270346111723422, 0.5230192003173261828, 0.5120000961863576672 ) ) 
 REPRESENTATION_ITEM ( '' )  );
#3239=CARTESIAN_POINT ( 'NONE',  ( 2.875000000000000888, 1.000000000000000222, -3.337500001222715174 ) ) ;
#3242=EDGE_CURVE ( 'NONE', #4502, #3161, #2072, .T. ) ;
#3254=ORIENTED_EDGE ( 'NONE', *, *, #878, .T. ) ;
#3258=DIRECTION ( 'NONE',  ( 0.000000000000000000, 0.000000000000000000, -1.000000000000000000 ) ) ;
#3283=FACE_OUTER_BOUND ( 'NONE', #2242, .T. ) ;
#3288=( BOUNDED_CURVE ( )  B_SPLINE_CURVE ( 3, ( #6903, #5542, #2560, #3042 ),
 .UNSPECIFIED., .F., .F. ) 
 B_SPLINE_CURVE_WITH_KNOTS ( ( 4, 4 ),
 ( 0.000000000000000000, 0.03896959986073553206 ),
 .UNSPECIFIED. ) 
 CURVE ( )  GEOMETRIC_REPRESENTATION_ITEM ( )  RATIONAL_B_SPLINE_CURVE ( ( 0.7490764964646237090, 0.6867990767679545971, 0.6362002288929724525, 0.5972799528396776081 ) ) 
 REPRESENTATION_ITEM ( '' )  );
#3299=DIRECTION ( 'NONE',  ( 0.9917930140139563644, 0.000000000000000000, -0.1278538906451900103 ) ) ;
#3304=VECTOR ( 'NONE', #1006, 39.37007874015748143 ) ;
#3322=VECTOR ( 'NONE', #5365, 39.37007874015748143 ) ;
#3327=DIRECTION ( 'NONE',  ( 0.000000000000000000, -1.000000000000000000, 0.000000000000000000 ) ) ;
#3329=VECTOR ( 'NONE', #3960, 39.37007874015748143 ) ;
#3334=DIRECTION ( 'NONE',  ( -0.000000000000000000, -1.000000000000000000, -0.000000000000000000 ) ) ;
#3356=CARTESIAN_POINT ( 'NONE',  ( 3.796513186599489220, 1.000000000000000444, -2.946478861041413211 ) ) ;
#3371=EDGE_CURVE ( 'NONE', #2528, #5154, #1218, .T. ) ;
#3372=DIRECTION ( 'NONE',  ( -0.3026345437736693289, 0.000000000000000000, 0.9531066744677130220 ) ) ;
#3375=VERTEX_POINT ( 'NONE', #8083 ) ;
#3376=CARTESIAN_POINT ( 'NONE',  ( -3.651126736336024692, 1.000000000000000444, -1.298036422402331302 ) ) ;
#3384=DIRECTION ( 'NONE',  ( -0.9961332539796342589, 0.000000000000000000, -0.08785522361217638909 ) ) ;
#3387=CARTESIAN_POINT ( 'NONE',  ( -3.687499989627467389, 1.000000000000000888, 3.874999999790589289 ) ) ;
#3394=EDGE_CURVE ( 'NONE', #605, #4681, #3943, .T. ) ;
#3397=VERTEX_POINT ( 'NONE', #5438 ) ;
#3400=FACE_OUTER_BOUND ( 'NONE', #2041, .T. ) ;
#3419=EDGE_CURVE ( 'NONE', #2413, #2164, #5171, .T. ) ;
#3423=FACE_OUTER_BOUND ( 'NONE', #5534, .T. ) ;
#3437=DIRECTION ( 'NONE',  ( -0.000000000000000000, 1.000000000000000000, -0.000000000000000000 ) ) ;
#3454=DIRECTION ( 'NONE',  ( -0.000000000000000000, -1.000000000000000000, -0.000000000000000000 ) ) ;
#3460=CIRCLE ( 'NONE', #2021, 3.874999999025058539 ) ;
#3463=VECTOR ( 'NONE', #1635, 39.37007874015748143 ) ;
#3478=VECTOR ( 'NONE', #5763, 39.37007874015748854 ) ;
#3479=VERTEX_POINT ( 'NONE', #563 ) ;
#3488=CARTESIAN_POINT ( 'NONE',  ( -3.562500000000000444, -3.820994442221351629E-18, 3.337500000000003020 ) ) ;
#3497=LINE ( 'NONE', #6000, #3322 ) ;
#3499=EDGE_CURVE ( 'NONE', #750, #7757, #6025, .T. ) ;
#3505=LINE ( 'NONE', #4103, #3221 ) ;
#3519=EDGE_LOOP ( 'NONE', ( #7711, #5494, #3254, #385 ) ) ;
#3536=EDGE_CURVE ( 'NONE', #987, #6365, #7003, .T. ) ;
#3537=CARTESIAN_POINT ( 'NONE',  ( -2.875000000000000888, 1.000000000000000222, -2.612499998777286780 ) ) ;
#3544=ORIENTED_EDGE ( 'NONE', *, *, #6740, .T. ) ;
#3549=EDGE_CURVE ( 'NONE', #4517, #2229, #3227, .T. ) ;
#3550=ORIENTED_EDGE ( 'NONE', *, *, #7046, .F. ) ;
#3551=DIRECTION ( 'NONE',  ( 0.9925485533564400997, 0.000000000000000000, -0.1218497814115311745 ) ) ;
#3552=ORIENTED_EDGE ( 'NONE', *, *, #5998, .F. ) ;
#3554=ORIENTED_EDGE ( 'NONE', *, *, #1381, .F. ) ;
#3557=DIRECTION ( 'NONE',  ( 0.000000000000000000, -1.000000000000000000, 0.000000000000000000 ) ) ;
#3579=DIRECTION ( 'NONE',  ( -0.000000000000000000, -1.000000000000000000, -0.000000000000000000 ) ) ;
#3587=AXIS2_PLACEMENT_3D ( 'NONE', #5420, #543, #5541 ) ;
#3588=CARTESIAN_POINT ( 'NONE',  ( -3.791570908345035740, 1.000000000000000222, 0.7997593681799637366 ) ) ;
#3589=ORIENTED_EDGE ( 'NONE', *, *, #3082, .T. ) ;
#3592=DIRECTION ( 'NONE',  ( -0.000000000000000000, 1.000000000000000000, -0.000000000000000000 ) ) ;
#3602=DIRECTION ( 'NONE',  ( -0.000000000000000000, -1.000000000000000000, -0.000000000000000000 ) ) ;
#3603=VECTOR ( 'NONE', #4381, 39.37007874015748143 ) ;
#3607=CARTESIAN_POINT ( 'NONE',  ( -2.637478091534712021, 0.9999999999981570298, -2.843572666449250441 ) ) ;
#3613=CARTESIAN_POINT ( 'NONE',  ( 2.513411990276540831, 1.000000000000000222, -2.949302488239232023 ) ) ;
#3617=CARTESIAN_POINT ( 'NONE',  ( 3.583510604133039124, 1.543025754838326824, -7.167021208266083576 ) ) ;
#3618=DIRECTION ( 'NONE',  ( 0.000000000000000000, 0.000000000000000000, -1.000000000000000000 ) ) ;
#3626=LINE ( 'NONE', #4270, #6845 ) ;
#3629=EDGE_CURVE ( 'NONE', #295, #2186, #4622, .T. ) ;
#3634=EDGE_LOOP ( 'NONE', ( #3933, #6853, #5841, #7040 ) ) ;
#3636=DIRECTION ( 'NONE',  ( 0.000000000000000000, 0.000000000000000000, -1.000000000000000000 ) ) ;
#3638=ORIENTED_EDGE ( 'NONE', *, *, #6036, .F. ) ;
#3662=ORIENTED_EDGE ( 'NONE', *, *, #7992, .T. ) ;
#3664=DIRECTION ( 'NONE',  ( 0.000000000000000000, 0.000000000000000000, -1.000000000000000000 ) ) ;
#3689=DIRECTION ( 'NONE',  ( -0.000000000000000000, 1.000000000000000000, -0.000000000000000000 ) ) ;
#3712=FACE_OUTER_BOUND ( 'NONE', #7836, .T. ) ;
#3721=DIRECTION ( 'NONE',  ( 0.000000000000000000, 0.000000000000000000, 1.000000000000000000 ) ) ;
#3723=EDGE_LOOP ( 'NONE', ( #4141, #3662 ) ) ;
#3735=EDGE_CURVE ( 'NONE', #2229, #6048, #5271, .T. ) ;
#3736=CARTESIAN_POINT ( 'NONE',  ( 0.000000000000000000, 0.000000000000000000, 0.000000000000000000 ) ) ;
#3750=ORIENTED_EDGE ( 'NONE', *, *, #388, .T. ) ;
#3758=FACE_OUTER_BOUND ( 'NONE', #1390, .T. ) ;
#3794=CARTESIAN_POINT ( 'NONE',  ( -8.751021560936518753E-10, 1.000000000000000222, 5.750408897959578548E-10 ) ) ;
#3798=DIRECTION ( 'NONE',  ( 0.000000000000000000, 0.000000000000000000, -1.000000000000000000 ) ) ;
#3850=ORIENTED_EDGE ( 'NONE', *, *, #2044, .T. ) ;
#3852=ORIENTED_EDGE ( 'NONE', *, *, #1210, .F. ) ;
#3861=EDGE_LOOP ( 'NONE', ( #1968, #485 ) ) ;
#3862=CIRCLE ( 'NONE', #1794, 0.3625000000000019318 ) ;
#3872=EDGE_LOOP ( 'NONE', ( #8057, #629, #7174, #6077 ) ) ;
#3873=CARTESIAN_POINT ( 'NONE',  ( 0.000000000000000000, 3.001975734461090560E-16, 0.000000000000000000 ) ) ;
#3874=CARTESIAN_POINT ( 'NONE',  ( 2.513411990276540831, 1.000000000000000222, -2.949302488239232023 ) ) ;
#3895=EDGE_LOOP ( 'NONE', ( #2616, #5784 ) ) ;
#3898=FACE_OUTER_BOUND ( 'NONE', #4438, .T. ) ;
#3899=VERTEX_POINT ( 'NONE', #1289 ) ;
#3929=EDGE_CURVE ( 'NONE', #5062, #2186, #2681, .T. ) ;
#3930=CARTESIAN_POINT ( 'NONE',  ( -3.362500000000002931, 1.750000000000000000, -6.725000000000002309 ) ) ;
#3933=ORIENTED_EDGE ( 'NONE', *, *, #3996, .F. ) ;
#3934=DIRECTION ( 'NONE',  ( 0.000000000000000000, -1.000000000000000000, 0.000000000000000000 ) ) ;
#3938=CYLINDRICAL_SURFACE ( 'NONE', #728, 0.3625000012227142521 ) ;
#3943=CIRCLE ( 'NONE', #1488, 0.3625000012227142521 ) ;
#3954=AXIS2_PLACEMENT_3D ( 'NONE', #583, #462, #7464 ) ;
#3955=AXIS2_PLACEMENT_3D ( 'NONE', #3873, #6388, #771 ) ;
#3959=VECTOR ( 'NONE', #1088, 39.37007874015748143 ) ;
#3960=DIRECTION ( 'NONE',  ( -0.000000000000000000, -1.000000000000000000, -0.000000000000000000 ) ) ;
#3962=( BOUNDED_CURVE ( )  B_SPLINE_CURVE ( 3, ( #3115, #5607, #16, #2423 ),
 .UNSPECIFIED., .F., .F. ) 
 B_SPLINE_CURVE_WITH_KNOTS ( ( 4, 4 ),
 ( 0.000000000000000000, 0.09552853956270015989 ),
 .UNSPECIFIED. ) 
 CURVE ( )  GEOMETRIC_REPRESENTATION_ITEM ( )  RATIONAL_B_SPLINE_CURVE ( ( 0.5192122202261599817, 0.5593999942402725356, 0.6626358111613523949, 0.8289196709893995596 ) ) 
 REPRESENTATION_ITEM ( '' )  );
#3973=CIRCLE ( 'NONE', #3198, 3.874999999025058539 ) ;
#3974=EDGE_CURVE ( 'NONE', #3397, #1533, #6500, .T. ) ;
#3982=ORIENTED_EDGE ( 'NONE', *, *, #817, .F. ) ;
#3984=AXIS2_PLACEMENT_3D ( 'NONE', #7998, #5473, #3016 ) ;
#3987=EDGE_LOOP ( 'NONE', ( #7128, #148, #4855, #6776 ) ) ;
#3996=EDGE_CURVE ( 'NONE', #1711, #5062, #1230, .T. ) ;
#3997=ORIENTED_EDGE ( 'NONE', *, *, #3499, .T. ) ;
#4004=CARTESIAN_POINT ( 'NONE',  ( -8.751021560936518753E-10, 1.000000000000000222, 5.750408897959578548E-10 ) ) ;
#4008=CIRCLE ( 'NONE', #7582, 3.874999999025058539 ) ;
#4012=CARTESIAN_POINT ( 'NONE',  ( 2.875000000000000888, 0.000000000000000000, -2.975000000000000977 ) ) ;
#4013=EDGE_CURVE ( 'NONE', #1080, #615, #6198, .T. ) ;
#4014=ORIENTED_EDGE ( 'NONE', *, *, #4834, .T. ) ;
#4023=ORIENTED_EDGE ( 'NONE', *, *, #743, .F. ) ;
#4026=CARTESIAN_POINT ( 'NONE',  ( -8.751021560936518753E-10, 1.365923996832131609E-16, 5.750408897959578548E-10 ) ) ;
#4027=DIRECTION ( 'NONE',  ( 0.000000000000000000, 1.000000000000000000, 0.000000000000000000 ) ) ;
#4032=DIRECTION ( 'NONE',  ( 0.000000000000000000, -1.000000000000000000, 0.000000000000000000 ) ) ;
#4041=FACE_OUTER_BOUND ( 'NONE', #936, .T. ) ;
#4084=CARTESIAN_POINT ( 'NONE',  ( -3.762484563843162100, 1.281112611882646579, 4.607714677951853639E-16 ) ) ;
#4085=VECTOR ( 'NONE', #1700, 39.37007874015748854 ) ;
#4087=ORIENTED_EDGE ( 'NONE', *, *, #601, .T. ) ;
#4088=AXIS2_PLACEMENT_3D ( 'NONE', #1693, #2349, #3618 ) ;
#4089=CARTESIAN_POINT ( 'NONE',  ( 2.875000000000000888, 1.000000000000000222, -2.975000000000000977 ) ) ;
#4091=VECTOR ( 'NONE', #3372, 39.37007874015748854 ) ;
#4099=VECTOR ( 'NONE', #2993, 39.37007874015748854 ) ;
#4100=B_SPLINE_CURVE_WITH_KNOTS ( 'NONE', 3,
 ( #7443, #2116, #275, #5804 ),
 .UNSPECIFIED., .F., .F.,
 ( 4, 4 ),
 ( 0.000000000000000000, 1.000000000000000000 ),
 .UNSPECIFIED. ) ;
#4103=CARTESIAN_POINT ( 'NONE',  ( -1.462953685981321916, 1.365923996832131609E-16, 3.588229579027113481 ) ) ;
#4107=LINE ( 'NONE', #4188, #2438 ) ;
#4118=AXIS2_PLACEMENT_3D ( 'NONE', #5311, #7312, #7997 ) ;
#4125=EDGE_CURVE ( 'NONE', #584, #5712, #2141, .T. ) ;
#4126=EDGE_CURVE ( 'NONE', #2528, #7021, #6694, .T. ) ;
#4141=ORIENTED_EDGE ( 'NONE', *, *, #3371, .T. ) ;
#4144=FACE_OUTER_BOUND ( 'NONE', #3519, .T. ) ;
#4148=CARTESIAN_POINT ( 'NONE',  ( -3.362500000000001155, 1.750000000000000444, 4.117874862132976456E-16 ) ) ;
#4154=DIRECTION ( 'NONE',  ( -0.000000000000000000, -1.000000000000000000, -0.000000000000000000 ) ) ;
#4155=ORIENTED_EDGE ( 'NONE', *, *, #3242, .T. ) ;
#4156=CARTESIAN_POINT ( 'NONE',  ( 3.562500000000000444, 1.000000000000000222, 3.337500000000003020 ) ) ;
#4168=EDGE_CURVE ( 'NONE', #1442, #6680, #3497, .T. ) ;
#4170=CARTESIAN_POINT ( 'NONE',  ( -3.583510604133039568, 1.543025754838326824, 7.167021208266081800 ) ) ;
#4176=DIRECTION ( 'NONE',  ( 4.440892098507806374E-15, 0.000000000000000000, 1.000000000000000000 ) ) ;
#4177=CARTESIAN_POINT ( 'NONE',  ( 3.362500000000000711, 1.750000000000000444, -4.117874862132976456E-16 ) ) ;
#4188=CARTESIAN_POINT ( 'NONE',  ( -4.470366334113919926, 1.365923996832131609E-16, 2.937534001674281914 ) ) ;
#4189=ORIENTED_EDGE ( 'NONE', *, *, #4953, .F. ) ;
#4191=CARTESIAN_POINT ( 'NONE',  ( -8.751021560936518753E-10, 1.365923996832131609E-16, 5.750408897959578548E-10 ) ) ;
#4196=CARTESIAN_POINT ( 'NONE',  ( 3.687499987877262519, 1.000000000000000222, 3.874999999790589289 ) ) ;
#4197=EDGE_LOOP ( 'NONE', ( #2626, #5974 ) ) ;
#4200=DIRECTION ( 'NONE',  ( 0.000000000000000000, 0.000000000000000000, 1.000000000000000000 ) ) ;
#4209=CARTESIAN_POINT ( 'NONE',  ( 3.762484563843159435, 1.281112611882646579, -7.524969127686321535 ) ) ;
#4216=ORIENTED_EDGE ( 'NONE', *, *, #7472, .T. ) ;
#4228=CARTESIAN_POINT ( 'NONE',  ( -1.462953685906409840, 1.000000000000000222, 3.588229579118171308 ) ) ;
#4234=AXIS2_PLACEMENT_3D ( 'NONE', #4567, #972, #4647 ) ;
#4236=ORIENTED_EDGE ( 'NONE', *, *, #4842, .F. ) ;
#4238=DIRECTION ( 'NONE',  ( -0.000000000000000000, -1.000000000000000000, -0.000000000000000000 ) ) ;
#4240=CARTESIAN_POINT ( 'NONE',  ( 3.651126734928074491, 1.365923996832131609E-16, -1.298036420927624057 ) ) ;
#4250=EDGE_CURVE ( 'NONE', #5456, #2112, #1195, .T. ) ;
#4260=CARTESIAN_POINT ( 'NONE',  ( -3.762484563843162100, 1.281112611882646579, 4.607714677951853639E-16 ) ) ;
#4261=CIRCLE ( 'NONE', #2176, 0.3625000012227142521 ) ;
#4270=CARTESIAN_POINT ( 'NONE',  ( 2.875000000000000888, 0.000000000000000000, -2.612499998777286780 ) ) ;
#4286=EDGE_LOOP ( 'NONE', ( #4189, #8050 ) ) ;
#4287=CARTESIAN_POINT ( 'NONE',  ( -1.462953685889704536, 1.365923996832131609E-16, 3.588229579064466712 ) ) ;
#4305=CARTESIAN_POINT ( 'NONE',  ( -1.674765981361497014, 0.9999999999999978906, -3.533905824818027508 ) ) ;
#4324=CARTESIAN_POINT ( 'NONE',  ( 1.462953684461641091, 1.365923996832131609E-16, 3.588229578933126440 ) ) ;
#4332=ORIENTED_EDGE ( 'NONE', *, *, #6093, .T. ) ;
#4335=CARTESIAN_POINT ( 'NONE',  ( -3.562500000000000444, -3.820994442221351629E-18, 2.975000000000000977 ) ) ;
#4339=CARTESIAN_POINT ( 'NONE',  ( -2.126102704745536975, 0.9999999999999980016, -3.279369616341864635 ) ) ;
#4340=ORIENTED_EDGE ( 'NONE', *, *, #3118, .F. ) ;
#4342=DIRECTION ( 'NONE',  ( 0.000000000000000000, -1.000000000000000000, 0.000000000000000000 ) ) ;
#4350=CARTESIAN_POINT ( 'NONE',  ( -3.562500000000000444, 0.000000000000000000, 2.975000000000000977 ) ) ;
#4363=EDGE_CURVE ( 'NONE', #8092, #5981, #4897, .T. ) ;
#4379=AXIS2_PLACEMENT_3D ( 'NONE', #400, #1676, #7345 ) ;
#4381=DIRECTION ( 'NONE',  ( -0.9925485533564400997, -0.000000000000000000, 0.1218497814115311745 ) ) ;
#4389=VECTOR ( 'NONE', #714, 39.37007874015748143 ) ;
#4391=ORIENTED_EDGE ( 'NONE', *, *, #1210, .T. ) ;
#4393=CIRCLE ( 'NONE', #869, 0.3625000012227142521 ) ;
#4412=DIRECTION ( 'NONE',  ( -0.000000000000000000, 1.000000000000000000, -0.000000000000000000 ) ) ;
#4427=ADVANCED_FACE ( 'NONE', ( #3158 ), #6316, .F. ) ;
#4437=LINE ( 'NONE', #2644, #6524 ) ;
#4438=EDGE_LOOP ( 'NONE', ( #5490, #6105, #1781, #2520 ) ) ;
#4446=ORIENTED_EDGE ( 'NONE', *, *, #2920, .T. ) ;
#4448=CARTESIAN_POINT ( 'NONE',  ( 4.470366332363715500, 1.000000000000000666, 2.937534001674282358 ) ) ;
#4450=DIRECTION ( 'NONE',  ( -0.000000000000000000, -1.000000000000000000, -0.000000000000000000 ) ) ;
#4453=DIRECTION ( 'NONE',  ( -0.000000000000000000, -1.000000000000000000, -0.000000000000000000 ) ) ;
#4473=DIRECTION ( 'NONE',  ( 0.000000000000000000, -1.000000000000000000, 0.000000000000000000 ) ) ;
#4481=AXIS2_PLACEMENT_3D ( 'NONE', #6423, #1510, #766 ) ;
#4482=DIRECTION ( 'NONE',  ( 0.000000000000000000, -0.000000000000000000, 1.000000000000000000 ) ) ;
#4502=VERTEX_POINT ( 'NONE', #745 ) ;
#4506=DIRECTION ( 'NONE',  ( -0.000000000000000000, 1.000000000000000000, -0.000000000000000000 ) ) ;
#4507=ORIENTED_EDGE ( 'NONE', *, *, #8079, .T. ) ;
#4517=VERTEX_POINT ( 'NONE', #3239 ) ;
#4522=AXIS2_PLACEMENT_3D ( 'NONE', #7892, #922, #5373 ) ;
#4530=ADVANCED_FACE ( 'NONE', ( #2631 ), #7656, .F. ) ;
#4534=CARTESIAN_POINT ( 'NONE',  ( 2.815000007187132613, 1.365923996832131609E-16, -3.895000001893597741 ) ) ;
#4535=CIRCLE ( 'NONE', #5844, 3.874999999025058539 ) ;
#4541=ORIENTED_EDGE ( 'NONE', *, *, #166, .T. ) ;
#4542=CARTESIAN_POINT ( 'NONE',  ( -2.815000008655330621, 1.365923996832131609E-16, -3.895000002097408487 ) ) ;
#4548=ORIENTED_EDGE ( 'NONE', *, *, #3082, .F. ) ;
#4567=CARTESIAN_POINT ( 'NONE',  ( -8.751021560936518753E-10, 1.365923996832131609E-16, 5.750408897959578548E-10 ) ) ;
#4588=EDGE_CURVE ( 'NONE', #605, #5981, #1480, .T. ) ;
#4591=DIRECTION ( 'NONE',  ( 0.000000000000000000, 0.000000000000000000, -1.000000000000000000 ) ) ;
#4597=MANIFOLD_SOLID_BREP ( 'Imported1', #2817 ) ;
#4599=CARTESIAN_POINT ( 'NONE',  ( 1.462953684461640202, 1.365923996832131609E-16, 3.588229578933126884 ) ) ;
#4603=APPLICATION_CONTEXT ( 'configuration controlled 3d designs of mechanical parts and assemblies' ) ;
#4612=ORIENTED_EDGE ( 'NONE', *, *, #5840, .F. ) ;
#4618=DIRECTION ( 'NONE',  ( 0.000000000000000000, 0.000000000000000000, 1.000000000000000000 ) ) ;
#4622=CIRCLE ( 'NONE', #3955, 2.845000000000001528 ) ;
#4630=CYLINDRICAL_SURFACE ( 'NONE', #2929, 0.3625000012227142521 ) ;
#4644=VECTOR ( 'NONE', #3299, 39.37007874015748143 ) ;
#4647=DIRECTION ( 'NONE',  ( 0.000000000000000000, 0.000000000000000000, 1.000000000000000000 ) ) ;
#4651=CARTESIAN_POINT ( 'NONE',  ( -8.751021560936518753E-10, 1.000000000000000222, 5.750408897959578548E-10 ) ) ;
#4657=CARTESIAN_POINT ( 'NONE',  ( 3.562500000000000444, -3.820994442221351629E-18, 2.975000000000000977 ) ) ;
#4660=DIRECTION ( 'NONE',  ( 0.000000000000000000, -0.000000000000000000, 1.000000000000000000 ) ) ;
#4665=AXIS2_PLACEMENT_3D ( 'NONE', #6972, #4342, #1284 ) ;
#4670=DIRECTION ( 'NONE',  ( -0.9531066744720206874, 0.000000000000000000, 0.3026345437601031252 ) ) ;
#4681=VERTEX_POINT ( 'NONE', #2903 ) ;
#4683=DIRECTION ( 'NONE',  ( -0.000000000000000000, 1.000000000000000000, -0.000000000000000000 ) ) ;
#4710=CARTESIAN_POINT ( 'NONE',  ( -3.875000000000001332, 1.000000000000000222, 7.750000000000002665 ) ) ;
#4712=EDGE_LOOP ( 'NONE', ( #1096, #1763 ) ) ;
#4713=CARTESIAN_POINT ( 'NONE',  ( -3.875000000000003109, 1.000000000000000222, -7.750000000000002665 ) ) ;
#4730=EDGE_CURVE ( 'NONE', #1442, #6928, #4917, .T. ) ;
#4737=CARTESIAN_POINT ( 'NONE',  ( -3.562500000000000444, 1.000000000000000222, 2.975000000000000977 ) ) ;
#4740=CARTESIAN_POINT ( 'NONE',  ( -2.513411990276539942, 1.000000000000000444, -2.949302488239234243 ) ) ;
#4744=DIRECTION ( 'NONE',  ( 0.000000000000000000, 0.000000000000000000, -1.000000000000000000 ) ) ;
#4749=CARTESIAN_POINT ( 'NONE',  ( 3.583510604133040900, 1.543025754838327046, -8.777069582124253846E-16 ) ) ;
#4752=VECTOR ( 'NONE', #5835, 39.37007874015748143 ) ;
#4759=( BOUNDED_SURFACE ( )  B_SPLINE_SURFACE ( 3, 3, ( 
 ( #2221, #2300, #4710, #4794 ),
 ( #7226, #7323, #1609, #4084 ),
 ( #6621, #7916, #4170, #6690 ),
 ( #6268, #5442, #3120, #8048 ) ),
 .UNSPECIFIED., .F., .F., .F. ) 
 B_SPLINE_SURFACE_WITH_KNOTS ( ( 4, 4 ),
 ( 4, 4 ),
 ( 0.000000000000000000, 1.000000000000000000 ),
 ( 0.000000000000000000, 1.000000000000000000 ),
 .UNSPECIFIED. ) 
 GEOMETRIC_REPRESENTATION_ITEM ( )  RATIONAL_B_SPLINE_SURFACE ( (
 ( 1.000000000000000000, 0.3333333333333334259, 0.3333333333333334259, 1.000000000000000000),
 ( 1.000000000000000000, 0.3333333333333334259, 0.3333333333333334259, 1.000000000000000000),
 ( 1.000000000000000000, 0.3333333333333334259, 0.3333333333333334259, 1.000000000000000000),
 ( 1.000000000000000000, 0.3333333333333334259, 0.3333333333333334259, 1.000000000000000000) ) ) 
 REPRESENTATION_ITEM ( '' )  SURFACE ( )  );
#4771=CARTESIAN_POINT ( 'NONE',  ( 3.362500000000000711, 1.750000000000000444, -4.117874862132976456E-16 ) ) ;
#4776=EDGE_CURVE ( 'NONE', #3375, #2544, #7453, .T. ) ;
#4778=CARTESIAN_POINT ( 'NONE',  ( 2.815000007187132613, 1.365923996832131609E-16, -3.895000001893597297 ) ) ;
#4785=LINE ( 'NONE', #6481, #5955 ) ;
#4787=CARTESIAN_POINT ( 'NONE',  ( 3.562500000000000444, -0.000000000000000000, 3.337500000000003020 ) ) ;
#4790=DIRECTION ( 'NONE',  ( -0.000000000000000000, -1.000000000000000000, -0.000000000000000000 ) ) ;
#4794=CARTESIAN_POINT ( 'NONE',  ( -3.875000000000002220, 1.000000000000000222, 4.745506346695996852E-16 ) ) ;
#4797=FACE_OUTER_BOUND ( 'NONE', #1852, .T. ) ;
#4798=CARTESIAN_POINT ( 'NONE',  ( 2.875000000000000888, 1.000000000000000222, -2.612499998777286780 ) ) ;
#4804=CARTESIAN_POINT ( 'NONE',  ( 1.462953684461641091, 1.365923996832131609E-16, 3.588229578933126884 ) ) ;
#4813=SHAPE_REPRESENTATION ( 'bench vise-', ( #7272 ), #3062 ) ;
#4820=DIRECTION ( 'NONE',  ( -0.000000000000000000, 1.000000000000000000, -0.000000000000000000 ) ) ;
#4834=EDGE_CURVE ( 'NONE', #5456, #3375, #2930, .T. ) ;
#4837=DIRECTION ( 'NONE',  ( -0.000000000000000000, -1.000000000000000000, -0.000000000000000000 ) ) ;
#4838=EDGE_CURVE ( 'NONE', #2112, #7591, #6267, .T. ) ;
#4842=EDGE_CURVE ( 'NONE', #2216, #4886, #3973, .T. ) ;
#4844=DIRECTION ( 'NONE',  ( -0.000000000000000000, -1.000000000000000000, -0.000000000000000000 ) ) ;
#4855=ORIENTED_EDGE ( 'NONE', *, *, #166, .F. ) ;
#4857=CYLINDRICAL_SURFACE ( 'NONE', #7446, 3.874999999025058539 ) ;
#4868=DIRECTION ( 'NONE',  ( -0.000000000000000000, -1.000000000000000000, -0.000000000000000000 ) ) ;
#4869=ORIENTED_EDGE ( 'NONE', *, *, #8016, .T. ) ;
#4871=CARTESIAN_POINT ( 'NONE',  ( 4.470366332363715500, 1.000000000000000888, 2.937534001674282358 ) ) ;
#4873=VERTEX_POINT ( 'NONE', #5074 ) ;
#4880=AXIS2_PLACEMENT_3D ( 'NONE', #4651, #4032, #6384 ) ;
#4886=VERTEX_POINT ( 'NONE', #2663 ) ;
#4888=VECTOR ( 'NONE', #3454, 39.37007874015748143 ) ;
#4895=EDGE_LOOP ( 'NONE', ( #5124, #2263, #2401, #5938 ) ) ;
#4897=CIRCLE ( 'NONE', #180, 0.3625000012227142521 ) ;
#4900=ORIENTED_EDGE ( 'NONE', *, *, #632, .F. ) ;
#4915=FACE_BOUND ( 'NONE', #6949, .T. ) ;
#4917=LINE ( 'NONE', #1809, #7270 ) ;
#4918=CARTESIAN_POINT ( 'NONE',  ( 2.815000007187132613, 1.000000000000000222, -3.895000001893597297 ) ) ;
#4925=AXIS2_PLACEMENT_3D ( 'NONE', #2894, #5386, #5470 ) ;
#4950=DIRECTION ( 'NONE',  ( -0.000000000000000000, 1.000000000000000000, 0.000000000000000000 ) ) ;
#4953=EDGE_CURVE ( 'NONE', #7021, #2549, #6992, .T. ) ;
#4959=LINE ( 'NONE', #7499, #7592 ) ;
#4960=ORIENTED_EDGE ( 'NONE', *, *, #6650, .T. ) ;
#4962=EDGE_LOOP ( 'NONE', ( #554, #7033, #1075, #6697 ) ) ;
#4964=ORIENTED_EDGE ( 'NONE', *, *, #5601, .T. ) ;
#4978=CARTESIAN_POINT ( 'NONE',  ( 0.000000000000000000, 3.001975734461090560E-16, -2.845000000000001528 ) ) ;
#4981=VERTEX_POINT ( 'NONE', #3356 ) ;
#4983=EDGE_CURVE ( 'NONE', #8139, #3899, #2822, .T. ) ;
#5002=EDGE_LOOP ( 'NONE', ( #917, #4507, #1708, #6550 ) ) ;
#5007=DIRECTION ( 'NONE',  ( -0.000000000000000000, -1.000000000000000000, -0.000000000000000000 ) ) ;
#5010=DIRECTION ( 'NONE',  ( -0.1218497812680350983, 0.000000000000000000, 0.9925485533740563415 ) ) ;
#5015=AXIS2_PLACEMENT_3D ( 'NONE', #7224, #4670, #6490 ) ;
#5019=DIRECTION ( 'NONE',  ( 0.000000000000000000, 0.000000000000000000, 1.000000000000000000 ) ) ;
#5026=EDGE_CURVE ( 'NONE', #7925, #1938, #7257, .T. ) ;
#5037=ORIENTED_EDGE ( 'NONE', *, *, #589, .T. ) ;
#5040=CARTESIAN_POINT ( 'NONE',  ( -2.875000000000000888, 1.000000000000000222, -2.975000000000000977 ) ) ;
#5046=ORIENTED_EDGE ( 'NONE', *, *, #5026, .T. ) ;
#5050=FACE_OUTER_BOUND ( 'NONE', #7571, .T. ) ;
#5061=DIRECTION ( 'NONE',  ( 0.9531066744677130220, 0.000000000000000000, 0.3026345437736693289 ) ) ;
#5062=VERTEX_POINT ( 'NONE', #2776 ) ;
#5064=CARTESIAN_POINT ( 'NONE',  ( -3.796513189164426816, 1.000000000000000888, -2.946478859991635169 ) ) ;
#5074=CARTESIAN_POINT ( 'NONE',  ( 2.815000007187131725, 1.365923996832131609E-16, -3.895000001893597741 ) ) ;
#5079=( BOUNDED_CURVE ( )  B_SPLINE_CURVE ( 3, ( #6804, #7403, #8090, #3613 ),
 .UNSPECIFIED., .F., .F. ) 
 B_SPLINE_CURVE_WITH_KNOTS ( ( 4, 4 ),
 ( 0.000000000000000000, 0.01230154035705741285 ),
 .UNSPECIFIED. ) 
 CURVE ( )  GEOMETRIC_REPRESENTATION_ITEM ( )  RATIONAL_B_SPLINE_CURVE ( ( 0.5972799528396778301, 0.5865781935274074765, 0.5767594089368136556, 0.5678235990678964784 ) ) 
 REPRESENTATION_ITEM ( '' )  );
#5080=ORIENTED_EDGE ( 'NONE', *, *, #4588, .F. ) ;
#5103=DIRECTION ( 'NONE',  ( 0.000000000000000000, 0.000000000000000000, 1.000000000000000000 ) ) ;
#5106=CARTESIAN_POINT ( 'NONE',  ( 3.651126734928074491, 1.365923996832131609E-16, -1.298036420927624501 ) ) ;
#5119=ADVANCED_FACE ( 'NONE', ( #8071 ), #1829, .F. ) ;
#5124=ORIENTED_EDGE ( 'NONE', *, *, #4168, .F. ) ;
#5125=ADVANCED_FACE ( 'NONE', ( #3712 ), #1753, .T. ) ;
#5128=CARTESIAN_POINT ( 'NONE',  ( 2.875000000000000888, -3.820994292482255198E-18, -2.975000000000000977 ) ) ;
#5154=VERTEX_POINT ( 'NONE', #4156 ) ;
#5156=CIRCLE ( 'NONE', #7827, 0.3625000000000019318 ) ;
#5163=VERTEX_POINT ( 'NONE', #4196 ) ;
#5171=( BOUNDED_CURVE ( )  B_SPLINE_CURVE ( 3, ( #1149, #3607, #6107, #527 ),
 .UNSPECIFIED., .F., .T. ) 
 B_SPLINE_CURVE_WITH_KNOTS ( ( 4, 4 ),
 ( 0.000000000000000000, 0.01230154035705745275 ),
 .UNSPECIFIED. ) 
 CURVE ( )  GEOMETRIC_REPRESENTATION_ITEM ( )  RATIONAL_B_SPLINE_CURVE ( ( 0.5678235990678963674, 0.5767594089368156540, 0.5865781935274119174, 0.5972799528396851576 ) ) 
 REPRESENTATION_ITEM ( '' )  );
#5175=VECTOR ( 'NONE', #7843, 39.37007874015748854 ) ;
#5176=CARTESIAN_POINT ( 'NONE',  ( -3.651126736044647547, 1.365923996832131609E-16, -1.298036422709905713 ) ) ;
#5178=ORIENTED_EDGE ( 'NONE', *, *, #6929, .F. ) ;
#5185=CIRCLE ( 'NONE', #6241, 0.3625000012227142521 ) ;
#5186=ORIENTED_EDGE ( 'NONE', *, *, #5840, .T. ) ;
#5201=DIRECTION ( 'NONE',  ( 0.000000000000000000, 0.000000000000000000, 1.000000000000000000 ) ) ;
#5202=ORIENTED_EDGE ( 'NONE', *, *, #4126, .T. ) ;
#5237=FACE_OUTER_BOUND ( 'NONE', #1775, .T. ) ;
#5241=DIRECTION ( 'NONE',  ( 0.000000000000000000, 0.000000000000000000, 1.000000000000000000 ) ) ;
#5243=CARTESIAN_POINT ( 'NONE',  ( 0.000000000000000000, 1.750000000000000444, 0.000000000000000000 ) ) ;
#5263=ORIENTED_EDGE ( 'NONE', *, *, #3394, .T. ) ;
#5271=CIRCLE ( 'NONE', #2797, 0.3625000012227142521 ) ;
#5279=ORIENTED_EDGE ( 'NONE', *, *, #784, .T. ) ;
#5311=CARTESIAN_POINT ( 'NONE',  ( 0.000000000000000000, 0.000000000000000000, -0.000000000000000000 ) ) ;
#5316=CIRCLE ( 'NONE', #1014, 4.805751768934915624 ) ;
#5320=CARTESIAN_POINT ( 'NONE',  ( -2.875000000000000888, 0.000000000000000000, -2.612499998777286780 ) ) ;
#5321=DIRECTION ( 'NONE',  ( -0.000000000000000000, -1.000000000000000000, -0.000000000000000000 ) ) ;
#5328=DIRECTION ( 'NONE',  ( 0.000000000000000000, 0.000000000000000000, -1.000000000000000000 ) ) ;
#5330=( BOUNDED_CURVE ( )  B_SPLINE_CURVE ( 3, ( #3588, #2969, #5462, #4228 ),
 .UNSPECIFIED., .F., .T. ) 
 B_SPLINE_CURVE_WITH_KNOTS ( ( 4, 4 ),
 ( 6.938893903907228378E-18, 0.09552853962307136793 ),
 .UNSPECIFIED. ) 
 CURVE ( )  GEOMETRIC_REPRESENTATION_ITEM ( )  RATIONAL_B_SPLINE_CURVE ( ( 0.8289196715399411719, 0.6626358114187893555, 0.5593999943213423531, 0.5192122202476002757 ) ) 
 REPRESENTATION_ITEM ( '' )  );
#5337=CARTESIAN_POINT ( 'NONE',  ( -3.796513189164427260, 1.365923996832131609E-16, -2.946478859991638277 ) ) ;
#5340=LINE ( 'NONE', #3387, #6877 ) ;
#5342=ADVANCED_FACE ( 'NONE', ( #3898 ), #7760, .T. ) ;
#5365=DIRECTION ( 'NONE',  ( 0.000000000000000000, 1.000000000000000000, -0.000000000000000000 ) ) ;
#5373=DIRECTION ( 'NONE',  ( 0.000000000000000000, 0.000000000000000000, 1.000000000000000000 ) ) ;
#5379=CARTESIAN_POINT ( 'NONE',  ( 2.815000007187133058, 1.000000000000000222, -3.895000001893596853 ) ) ;
#5382=ORIENTED_EDGE ( 'NONE', *, *, #3735, .T. ) ;
#5386=DIRECTION ( 'NONE',  ( -0.000000000000000000, -1.000000000000000000, -0.000000000000000000 ) ) ;
#5396=DIRECTION ( 'NONE',  ( 0.000000000000000000, 1.000000000000000000, 0.000000000000000000 ) ) ;
#5403=CARTESIAN_POINT ( 'NONE',  ( -3.762484563843162988, 1.281112611882646579, -7.524969127686321535 ) ) ;
#5405=ADVANCED_FACE ( 'NONE', ( #3423 ), #2848, .T. ) ;
#5407=DIRECTION ( 'NONE',  ( 0.000000000000000000, -1.000000000000000000, 0.000000000000000000 ) ) ;
#5410=ORIENTED_EDGE ( 'NONE', *, *, #6849, .F. ) ;
#5415=B_SPLINE_CURVE_WITH_KNOTS ( 'NONE', 3,
 ( #1770, #4260, #7229, #5999 ),
 .UNSPECIFIED., .F., .F.,
 ( 4, 4 ),
 ( 0.000000000000000000, 1.000000000000000000 ),
 .UNSPECIFIED. ) ;
#5420=CARTESIAN_POINT ( 'NONE',  ( -8.751021560936518753E-10, 1.365923996832131609E-16, 5.750408897959578548E-10 ) ) ;
#5433=EDGE_CURVE ( 'NONE', #8139, #1295, #6594, .T. ) ;
#5435=DIRECTION ( 'NONE',  ( 0.000000000000000000, -1.000000000000000000, 0.000000000000000000 ) ) ;
#5438=CARTESIAN_POINT ( 'NONE',  ( -3.791570908345035740, 1.365923996832131609E-16, 0.7997593681799632925 ) ) ;
#5442=CARTESIAN_POINT ( 'NONE',  ( 3.362500000000001155, 1.750000000000000222, 6.725000000000002309 ) ) ;
#5443=AXIS2_PLACEMENT_3D ( 'NONE', #638, #5010, #1253 ) ;
#5453=LINE ( 'NONE', #299, #5175 ) ;
#5456=VERTEX_POINT ( 'NONE', #2727 ) ;
#5462=CARTESIAN_POINT ( 'NONE',  ( -2.778020868884695460, 1.000000000000000000, 3.052064782510599095 ) ) ;
#5468=DIRECTION ( 'NONE',  ( 0.000000000000000000, 0.000000000000000000, -1.000000000000000000 ) ) ;
#5470=DIRECTION ( 'NONE',  ( 0.000000000000000000, 0.000000000000000000, -1.000000000000000000 ) ) ;
#5473=DIRECTION ( 'NONE',  ( -0.000000000000000000, -1.000000000000000000, -0.000000000000000000 ) ) ;
#5478=ADVANCED_FACE ( 'NONE', ( #797 ), #1506, .F. ) ;
#5490=ORIENTED_EDGE ( 'NONE', *, *, #4842, .T. ) ;
#5494=ORIENTED_EDGE ( 'NONE', *, *, #4168, .T. ) ;
#5500=CARTESIAN_POINT ( 'NONE',  ( 3.651126734928074491, 1.365923996832131609E-16, -1.298036420927624501 ) ) ;
#5502=ORIENTED_EDGE ( 'NONE', *, *, #3996, .T. ) ;
#5507=EDGE_CURVE ( 'NONE', #987, #7723, #1623, .T. ) ;
#5508=CARTESIAN_POINT ( 'NONE',  ( 2.875000000000000888, -3.820994292482255198E-18, -3.337500001222715174 ) ) ;
#5510=ORIENTED_EDGE ( 'NONE', *, *, #1163, .T. ) ;
#5518=ORIENTED_EDGE ( 'NONE', *, *, #5507, .F. ) ;
#5523=ORIENTED_EDGE ( 'NONE', *, *, #3023, .F. ) ;
#5526=AXIS2_PLACEMENT_3D ( 'NONE', #6289, #4473, #3136 ) ;
#5534=EDGE_LOOP ( 'NONE', ( #325, #1472, #4014, #854 ) ) ;
#5541=DIRECTION ( 'NONE',  ( 0.000000000000000000, 0.000000000000000000, 1.000000000000000000 ) ) ;
#5542=CARTESIAN_POINT ( 'NONE',  ( 3.484361157547035681, 0.9999999999999639178, -1.767115912903641339 ) ) ;
#5545=AXIS2_PLACEMENT_3D ( 'NONE', #4657, #2124, #855 ) ;
#5546=CARTESIAN_POINT ( 'NONE',  ( -3.362499999999999822, 1.750000000000000222, 6.725000000000002309 ) ) ;
#5547=APPLICATION_CONTEXT ( 'configuration controlled 3d designs of mechanical parts and assemblies' ) ;
#5551=CIRCLE ( 'NONE', #7422, 2.845000000000001528 ) ;
#5552=CARTESIAN_POINT ( 'NONE',  ( -2.815000008655331509, 1.000000000000000444, -3.895000002097408043 ) ) ;
#5557=CARTESIAN_POINT ( 'NONE',  ( -8.751021560936518753E-10, 1.000000000000000222, 5.750408897959578548E-10 ) ) ;
#5559=VECTOR ( 'NONE', #3602, 39.37007874015748143 ) ;
#5567=CARTESIAN_POINT ( 'NONE',  ( 0.000000000000000000, 0.000000000000000000, -0.000000000000000000 ) ) ;
#5574=ORIENTED_EDGE ( 'NONE', *, *, #7159, .T. ) ;
#5575=CARTESIAN_POINT ( 'NONE',  ( -3.562500000000000444, -3.820994442221351629E-18, 2.612499999999998934 ) ) ;
#5580=CARTESIAN_POINT ( 'NONE',  ( 0.000000000000000000, 3.001975734461090560E-16, 0.000000000000000000 ) ) ;
#5582=ADVANCED_FACE ( 'NONE', ( #4144 ), #6164, .T. ) ;
#5590=ORIENTED_EDGE ( 'NONE', *, *, #6984, .T. ) ;
#5601=EDGE_CURVE ( 'NONE', #4502, #7088, #5330, .T. ) ;
#5604=CARTESIAN_POINT ( 'NONE',  ( 2.815000007187132613, 1.365923996832131609E-16, -3.895000001893597297 ) ) ;
#5607=CARTESIAN_POINT ( 'NONE',  ( 2.778020867214854750, 1.000000000000000000, 3.052064783514492063 ) ) ;
#5608=ORIENTED_EDGE ( 'NONE', *, *, #4834, .F. ) ;
#5618=DIRECTION ( 'NONE',  ( 1.000000000000000000, 0.000000000000000000, 0.000000000000000000 ) ) ;
#5620=EDGE_LOOP ( 'NONE', ( #5935, #3170, #715, #7900 ) ) ;
#5628=ORIENTED_EDGE ( 'NONE', *, *, #926, .F. ) ;
#5633=ORIENTED_EDGE ( 'NONE', *, *, #3419, .T. ) ;
#5635=DIRECTION ( 'NONE',  ( -0.000000000000000000, -1.000000000000000000, -0.000000000000000000 ) ) ;
#5643=DIRECTION ( 'NONE',  ( -0.000000000000000000, 1.000000000000000000, -0.000000000000000000 ) ) ;
#5656=CIRCLE ( 'NONE', #7664, 5.349138356872925826 ) ;
#5669=AXIS2_PLACEMENT_3D ( 'NONE', #5243, #6545, #1043 ) ;
#5673=FACE_OUTER_BOUND ( 'NONE', #7649, .T. ) ;
#5675=DIRECTION ( 'NONE',  ( 0.000000000000000000, 1.000000000000000000, -0.000000000000000000 ) ) ;
#5691=DIRECTION ( 'NONE',  ( -0.000000000000000000, -1.000000000000000000, -0.000000000000000000 ) ) ;
#5696=CARTESIAN_POINT ( 'NONE',  ( -4.470366334113919926, 1.365923996832131609E-16, 2.937534001674282358 ) ) ;
#5699=DIMENSIONAL_EXPONENTS ( 1.000000000000000000, 0.000000000000000000, 0.000000000000000000, 0.000000000000000000, 0.000000000000000000, 0.000000000000000000, 0.000000000000000000 ) ;
#5701=CARTESIAN_POINT ( 'NONE',  ( -3.796513189164425928, 1.365923996832131609E-16, -2.946478859991638277 ) ) ;
#5711=LINE ( 'NONE', #6502, #4389 ) ;
#5712=VERTEX_POINT ( 'NONE', #2594 ) ;
#5713=CARTESIAN_POINT ( 'NONE',  ( 3.687499987877263408, 1.365923996832131609E-16, 3.874999999790588401 ) ) ;
#5720=VECTOR ( 'NONE', #1680, 39.37007874015748143 ) ;
#5721=FACE_BOUND ( 'NONE', #4712, .T. ) ;
#5737=ADVANCED_FACE ( 'N', ( #3283 ), #5781, .F. ) ;
#5749=ORIENTED_EDGE ( 'NONE', *, *, #776, .F. ) ;
#5751=EDGE_CURVE ( 'NONE', #2544, #2688, #3460, .T. ) ;
#5761=ORIENTED_EDGE ( 'NONE', *, *, #1489, .T. ) ;
#5763=DIRECTION ( 'NONE',  ( 0.08785522444269551479, -0.000000000000000000, 0.9961332539063855185 ) ) ;
#5772=ORIENTED_EDGE ( 'NONE', *, *, #3974, .F. ) ;
#5781=PLANE ( 'NONE',  #1110 ) ;
#5783=DIRECTION ( 'NONE',  ( -0.1278538906451907875, 0.000000000000000000, -0.9917930140139562534 ) ) ;
#5784=ORIENTED_EDGE ( 'NONE', *, *, #4013, .T. ) ;
#5794=( BOUNDED_CURVE ( )  B_SPLINE_CURVE ( 3, ( #2913, #916, #1575, #8017 ),
 .UNSPECIFIED., .F., .T. ) 
 B_SPLINE_CURVE_WITH_KNOTS ( ( 4, 4 ),
 ( 1.387778780781445676E-17, 0.03896959987227040928 ),
 .UNSPECIFIED. ) 
 CURVE ( )  GEOMETRIC_REPRESENTATION_ITEM ( )  RATIONAL_B_SPLINE_CURVE ( ( 0.5972799528396773860, 0.6362002289060533222, 0.6867990768019666126, 0.7490764965274174791 ) ) 
 REPRESENTATION_ITEM ( '' )  );
#5795=DIRECTION ( 'NONE',  ( -0.000000000000000000, -1.000000000000000000, -0.000000000000000000 ) ) ;
#5804=CARTESIAN_POINT ( 'NONE',  ( 3.874999998766638587, 1.000000000000000222, -3.894564048797845777E-16 ) ) ;
#5808=ADVANCED_FACE ( 'NONE', ( #2132 ), #4630, .F. ) ;
#5810=VERTEX_POINT ( 'NONE', #455 ) ;
#5819=ORIENTED_EDGE ( 'NONE', *, *, #3023, .T. ) ;
#5827=CARTESIAN_POINT ( 'NONE',  ( -8.751021560936518753E-10, 1.365923996832131609E-16, 5.750408897959578548E-10 ) ) ;
#5835=DIRECTION ( 'NONE',  ( -0.000000000000000000, -1.000000000000000000, -0.000000000000000000 ) ) ;
#5836=AXIS2_PLACEMENT_3D ( 'NONE', #4350, #5007, #7431 ) ;
#5839=ADVANCED_FACE ( 'NONE', ( #5237 ), #7142, .F. ) ;
#5840=EDGE_CURVE ( 'NONE', #4981, #7723, #2182, .T. ) ;
#5841=ORIENTED_EDGE ( 'NONE', *, *, #3629, .T. ) ;
#5844=AXIS2_PLACEMENT_3D ( 'NONE', #3045, #1791, #8113 ) ;
#5850=CIRCLE ( 'NONE', #7848, 4.805751768934915624 ) ;
#5856=VECTOR ( 'NONE', #7045, 39.37007874015748854 ) ;
#5863=DIRECTION ( 'NONE',  ( 0.000000000000000000, -0.000000000000000000, 1.000000000000000000 ) ) ;
#5881=EDGE_LOOP ( 'NONE', ( #7498, #6806, #7624, #6960 ) ) ;
#5905=ORIENTED_EDGE ( 'NONE', *, *, #5507, .T. ) ;
#5921=ADVANCED_FACE ( 'NONE', ( #7833 ), #4759, .T. ) ;
#5935=ORIENTED_EDGE ( 'NONE', *, *, #2836, .F. ) ;
#5938=ORIENTED_EDGE ( 'NONE', *, *, #6042, .F. ) ;
#5945=VECTOR ( 'NONE', #496, 39.37007874015748143 ) ;
#5952=AXIS2_PLACEMENT_3D ( 'NONE', #4324, #2893, #6826 ) ;
#5955=VECTOR ( 'NONE', #2982, 39.37007874015748143 ) ;
#5956=DIRECTION ( 'NONE',  ( 0.000000000000000000, 0.000000000000000000, -1.000000000000000000 ) ) ;
#5957=EDGE_CURVE ( 'NONE', #3479, #5810, #5079, .T. ) ;
#5967=DIRECTION ( 'NONE',  ( 0.000000000000000000, -1.000000000000000000, 0.000000000000000000 ) ) ;
#5974=ORIENTED_EDGE ( 'NONE', *, *, #589, .F. ) ;
#5979=DIRECTION ( 'NONE',  ( 0.08785522444269371067, 0.000000000000000000, 0.9961332539063856295 ) ) ;
#5981=VERTEX_POINT ( 'NONE', #2952 ) ;
#5983=FACE_BOUND ( 'NONE', #3895, .T. ) ;
#5988=AXIS2_PLACEMENT_3D ( 'NONE', #1712, #4238, #5468 ) ;
#5998=EDGE_CURVE ( 'NONE', #5062, #1711, #2552, .T. ) ;
#5999=CARTESIAN_POINT ( 'NONE',  ( -3.362500000000001155, 1.750000000000000444, 4.117874862132976456E-16 ) ) ;
#6000=CARTESIAN_POINT ( 'NONE',  ( 4.470366332363715500, 1.365923996832131609E-16, 2.937534001674281914 ) ) ;
#6005=CARTESIAN_POINT ( 'NONE',  ( -3.687499989627468722, 1.365923996832131609E-16, 3.874999999790588401 ) ) ;
#6009=DIRECTION ( 'NONE',  ( 0.9961332539063856295, 0.000000000000000000, -0.08785522444269552866 ) ) ;
#6013=CARTESIAN_POINT ( 'NONE',  ( -3.874999999933440797, 1.000000000000000222, -5.476399496138180442E-16 ) ) ;
#6019=FACE_OUTER_BOUND ( 'NONE', #1437, .T. ) ;
#6025=LINE ( 'NONE', #2902, #25 ) ;
#6036=EDGE_CURVE ( 'NONE', #1469, #2357, #7824, .T. ) ;
#6042=EDGE_CURVE ( 'NONE', #6680, #5712, #8134, .T. ) ;
#6043=ORIENTED_EDGE ( 'NONE', *, *, #2920, .F. ) ;
#6046=DIRECTION ( 'NONE',  ( -0.000000000000000000, -1.000000000000000000, -0.000000000000000000 ) ) ;
#6048=VERTEX_POINT ( 'NONE', #6724 ) ;
#6059=EDGE_CURVE ( 'NONE', #1840, #1442, #2432, .T. ) ;
#6067=DIRECTION ( 'NONE',  ( -0.000000000000000000, -1.000000000000000000, -0.000000000000000000 ) ) ;
#6075=CARTESIAN_POINT ( 'NONE',  ( -1.172489671586611548, 1.000000000000000888, -3.693357951819908891 ) ) ;
#6077=ORIENTED_EDGE ( 'NONE', *, *, #4126, .F. ) ;
#6080=AXIS2_PLACEMENT_3D ( 'NONE', #885, #3384, #269 ) ;
#6085=DIRECTION ( 'NONE',  ( 0.000000000000000000, 0.000000000000000000, 1.000000000000000000 ) ) ;
#6093=EDGE_CURVE ( 'NONE', #6966, #3375, #6230, .T. ) ;
#6105=ORIENTED_EDGE ( 'NONE', *, *, #6413, .T. ) ;
#6107=CARTESIAN_POINT ( 'NONE',  ( -2.753607252840604147, 0.9999999999981570298, -2.731109880590406824 ) ) ;
#6109=DIRECTION ( 'NONE',  ( -0.3026345437601031807, 0.000000000000000000, -0.9531066744720204653 ) ) ;
#6113=CIRCLE ( 'NONE', #4665, 5.349138356872925826 ) ;
#6115=CARTESIAN_POINT ( 'NONE',  ( 3.362500000000000711, 1.750000000000000444, -8.235749724265952913E-16 ) ) ;
#6116=ORIENTED_EDGE ( 'NONE', *, *, #4730, .F. ) ;
#6117=CIRCLE ( 'NONE', #2587, 0.3625000012227142521 ) ;
#6119=CARTESIAN_POINT ( 'NONE',  ( -2.875000000000000888, -3.820994292482255198E-18, -3.337500001222715174 ) ) ;
#6127=CARTESIAN_POINT ( 'NONE',  ( 3.796513186599488776, 1.365923996832131609E-16, -2.946478861041413211 ) ) ;
#6154=ORIENTED_EDGE ( 'NONE', *, *, #3929, .T. ) ;
#6158=ORIENTED_EDGE ( 'NONE', *, *, #675, .F. ) ;
#6161=ORIENTED_EDGE ( 'NONE', *, *, #1163, .F. ) ;
#6164=CYLINDRICAL_SURFACE ( 'NONE', #3587, 5.349138356872925826 ) ;
#6170=ORIENTED_EDGE ( 'NONE', *, *, #1381, .T. ) ;
#6193=AXIS2_PLACEMENT_3D ( 'NONE', #2296, #4868, #2340 ) ;
#6198=CIRCLE ( 'NONE', #1751, 0.3625000000000019318 ) ;
#6230=LINE ( 'NONE', #4918, #3603 ) ;
#6233=ORIENTED_EDGE ( 'NONE', *, *, #6984, .F. ) ;
#6237=DIRECTION ( 'NONE',  ( 0.000000000000000000, 0.000000000000000000, 1.000000000000000000 ) ) ;
#6239=VERTEX_POINT ( 'NONE', #6963 ) ;
#6241=AXIS2_PLACEMENT_3D ( 'NONE', #1302, #4450, #2499 ) ;
#6242=AXIS2_PLACEMENT_3D ( 'NONE', #6448, #3327, #5241 ) ;
#6251=ORIENTED_EDGE ( 'NONE', *, *, #4125, .F. ) ;
#6252=ADVANCED_FACE ( 'NONE', ( #6312 ), #693, .F. ) ;
#6253=ADVANCED_FACE ( 'NONE', ( #3400 ), #2214, .T. ) ;
#6254=FACE_OUTER_BOUND ( 'NONE', #365, .T. ) ;
#6259=CYLINDRICAL_SURFACE ( 'NONE', #6872, 4.805751768934915624 ) ;
#6261=CARTESIAN_POINT ( 'NONE',  ( 3.562500000000000444, 1.000000000000000222, 2.612499999999998934 ) ) ;
#6267=LINE ( 'NONE', #4542, #7554 ) ;
#6268=CARTESIAN_POINT ( 'NONE',  ( 3.362500000000000711, 1.750000000000000444, 0.000000000000000000 ) ) ;
#6277=ADVANCED_FACE ( 'NONE', ( #4041 ), #7870, .T. ) ;
#6283=CARTESIAN_POINT ( 'NONE',  ( 2.875000000000000888, -3.820994292482255198E-18, -2.975000000000000977 ) ) ;
#6285=EDGE_CURVE ( 'NONE', #615, #1080, #5156, .T. ) ;
#6289=CARTESIAN_POINT ( 'NONE',  ( -8.751021560936518753E-10, 1.000000000000000222, 5.750408897959578548E-10 ) ) ;
#6301=CARTESIAN_POINT ( 'NONE',  ( 3.484120143574221651E-16, 3.001975734461090560E-16, 2.845000000000001528 ) ) ;
#6302=CARTESIAN_POINT ( 'NONE',  ( -3.562500000000000444, -3.820994442221351629E-18, 2.975000000000000977 ) ) ;
#6307=CARTESIAN_POINT ( 'NONE',  ( 1.172489671196043304, 1.000000000000000444, -3.693357952326151494 ) ) ;
#6308=FACE_OUTER_BOUND ( 'NONE', #7380, .T. ) ;
#6310=DIRECTION ( 'NONE',  ( 0.000000000000000000, 0.000000000000000000, 1.000000000000000000 ) ) ;
#6312=FACE_OUTER_BOUND ( 'NONE', #1174, .T. ) ;
#6316=PLANE ( 'NONE',  #1235 ) ;
#6323=ADVANCED_FACE ( 'NONE', ( #6019, #5983 ), #322, .T. ) ;
#6324=CIRCLE ( 'NONE', #4880, 3.874999999025058539 ) ;
#6330=EDGE_LOOP ( 'NONE', ( #7718, #7943, #1636, #566, #1067, #4548 ) ) ;
#6338=ORIENTED_EDGE ( 'NONE', *, *, #1489, .F. ) ;
#6341=PLANE ( 'NONE',  #463 ) ;
#6348=CARTESIAN_POINT ( 'NONE',  ( 2.126102704337182736, 1.000000000000000444, -3.279369616689862710 ) ) ;
#6349=AXIS2_PLACEMENT_3D ( 'NONE', #2778, #3437, #4618 ) ;
#6365=VERTEX_POINT ( 'NONE', #989 ) ;
#6384=DIRECTION ( 'NONE',  ( -2.664535259084986204E-15, 0.000000000000000000, 1.000000000000000000 ) ) ;
#6386=DIRECTION ( 'NONE',  ( -0.000000000000000000, 1.000000000000000000, 0.000000000000000000 ) ) ;
#6388=DIRECTION ( 'NONE',  ( -0.000000000000000000, -1.000000000000000000, -0.000000000000000000 ) ) ;
#6398=EDGE_CURVE ( 'NONE', #5712, #6928, #362, .T. ) ;
#6402=( NAMED_UNIT ( * ) PLANE_ANGLE_UNIT ( ) SI_UNIT ( $, .RADIAN. ) );
#6406=ORIENTED_EDGE ( 'NONE', *, *, #317, .T. ) ;
#6413=EDGE_CURVE ( 'NONE', #4886, #1701, #4785, .T. ) ;
#6423=CARTESIAN_POINT ( 'NONE',  ( 3.562500000000000444, -0.000000000000000000, 2.975000000000000977 ) ) ;
#6425=DIRECTION ( 'NONE',  ( -3.552713678812811104E-15, 0.000000000000000000, 1.000000000000000000 ) ) ;
#6443=CARTESIAN_POINT ( 'NONE',  ( 2.875000000000000888, 1.000000000000000222, -2.975000000000000977 ) ) ;
#6448=CARTESIAN_POINT ( 'NONE',  ( -8.751021560936518753E-10, 1.000000000000000222, 5.750408897959578548E-10 ) ) ;
#6451=( BOUNDED_CURVE ( )  B_SPLINE_CURVE ( 3, ( #4771, #3006, #5546, #4148 ),
 .UNSPECIFIED., .F., .F. ) 
 B_SPLINE_CURVE_WITH_KNOTS ( ( 4, 4 ),
 ( 1.016459758734699301E-17, 0.2669680800879517535 ),
 .UNSPECIFIED. ) 
 CURVE ( )  GEOMETRIC_REPRESENTATION_ITEM ( )  RATIONAL_B_SPLINE_CURVE ( ( 1.000000000000000000, 0.3333333333333334259, 0.3333333333333334259, 1.000000000000000000 ) ) 
 REPRESENTATION_ITEM ( '' )  );
#6452=EDGE_CURVE ( 'NONE', #4681, #8092, #1835, .T. ) ;
#6474=PRODUCT_DEFINITION_SHAPE ( 'NONE', 'NONE',  #6586 ) ;
#6481=CARTESIAN_POINT ( 'NONE',  ( -8.751021560936518753E-10, 1.365923996832131609E-16, 3.874999999600099443 ) ) ;
#6488=AXIS2_PLACEMENT_3D ( 'NONE', #7854, #2154, #2200 ) ;
#6490=DIRECTION ( 'NONE',  ( 0.3026345437601030697, 0.000000000000000000, 0.9531066744720204653 ) ) ;
#6500=LINE ( 'NONE', #874, #4091 ) ;
#6502=CARTESIAN_POINT ( 'NONE',  ( -3.562500000000000444, 0.000000000000000000, 3.337500000000003020 ) ) ;
#6509=DIRECTION ( 'NONE',  ( -0.3026345437736693289, -0.000000000000000000, 0.9531066744677130220 ) ) ;
#6517=EDGE_CURVE ( 'NONE', #1993, #7244, #7276, .T. ) ;
#6524=VECTOR ( 'NONE', #89, 39.37007874015748143 ) ;
#6545=DIRECTION ( 'NONE',  ( -0.000000000000000000, -1.000000000000000000, -0.000000000000000000 ) ) ;
#6550=ORIENTED_EDGE ( 'NONE', *, *, #1173, .F. ) ;
#6553=EDGE_CURVE ( 'NONE', #5810, #4517, #7015, .T. ) ;
#6566=PLANE ( 'NONE',  #342 ) ;
#6586=PRODUCT_DEFINITION ( 'UNKNOWN', '', #1164, #1368 ) ;
#6592=DIRECTION ( 'NONE',  ( 0.000000000000000000, 0.000000000000000000, -1.000000000000000000 ) ) ;
#6594=LINE ( 'NONE', #5337, #7559 ) ;
#6605=ADVANCED_FACE ( 'NONE', ( #7683 ), #6341, .T. ) ;
#6614=MECHANICAL_CONTEXT ( 'NONE', #5547, 'mechanical' ) ;
#6621=CARTESIAN_POINT ( 'NONE',  ( 3.583510604133040900, 1.543025754838327046, 0.000000000000000000 ) ) ;
#6637=PLANE ( 'NONE',  #2827 ) ;
#6646=DIRECTION ( 'NONE',  ( 0.000000000000000000, 0.000000000000000000, -1.000000000000000000 ) ) ;
#6649=AXIS2_PLACEMENT_3D ( 'NONE', #3010, #4820, #8029 ) ;
#6650=EDGE_CURVE ( 'NONE', #2357, #1469, #7703, .T. ) ;
#6655=DIRECTION ( 'NONE',  ( 0.000000000000000000, -1.000000000000000000, 0.000000000000000000 ) ) ;
#6657=EDGE_LOOP ( 'NONE', ( #1352, #1177, #80, #7895 ) ) ;
#6659=EDGE_CURVE ( 'NONE', #1295, #7244, #97, .T. ) ;
#6680=VERTEX_POINT ( 'NONE', #4448 ) ;
#6690=CARTESIAN_POINT ( 'NONE',  ( -3.583510604133041344, 1.543025754838327046, 4.388534791062126923E-16 ) ) ;
#6693=CARTESIAN_POINT ( 'NONE',  ( 3.875000000000000000, 1.000000000000000222, -7.750000000000002665 ) ) ;
#6694=LINE ( 'NONE', #261, #4888 ) ;
#6695=DIRECTION ( 'NONE',  ( 0.000000000000000000, 0.000000000000000000, -1.000000000000000000 ) ) ;
#6697=ORIENTED_EDGE ( 'NONE', *, *, #4250, .F. ) ;
#6702=CARTESIAN_POINT ( 'NONE',  ( -2.875000000000000888, 1.000000000000000222, -2.975000000000000977 ) ) ;
#6705=ORIENTED_EDGE ( 'NONE', *, *, #3211, .F. ) ;
#6719=VECTOR ( 'NONE', #6509, 39.37007874015748143 ) ;
#6724=CARTESIAN_POINT ( 'NONE',  ( 2.875000000000000888, -3.820994292482255198E-18, -2.612499998777286780 ) ) ;
#6740=EDGE_CURVE ( 'NONE', #750, #2216, #7603, .T. ) ;
#6758=ADVANCED_FACE ( 'NONE', ( #3758 ), #6259, .T. ) ;
#6775=DIRECTION ( 'NONE',  ( 0.9917930140014037388, 0.000000000000000000, 0.1278538907425630367 ) ) ;
#6776=ORIENTED_EDGE ( 'NONE', *, *, #6659, .F. ) ;
#6780=DIRECTION ( 'NONE',  ( -0.000000000000000000, -1.000000000000000000, -0.000000000000000000 ) ) ;
#6786=DIRECTION ( 'NONE',  ( -0.000000000000000000, 1.000000000000000000, -0.000000000000000000 ) ) ;
#6795=ADVANCED_FACE ( 'NONE', ( #7080 ), #3938, .F. ) ;
#6804=CARTESIAN_POINT ( 'NONE',  ( 2.861675873811764248, 1.000000000000000222, -2.612744953730403719 ) ) ;
#6806=ORIENTED_EDGE ( 'NONE', *, *, #3974, .T. ) ;
#6823=LINE ( 'NONE', #5713, #2838 ) ;
#6826=DIRECTION ( 'NONE',  ( -0.9917930140014037388, 0.000000000000000000, -0.1278538907425633420 ) ) ;
#6839=ORIENTED_EDGE ( 'NONE', *, *, #7928, .F. ) ;
#6845=VECTOR ( 'NONE', #3579, 39.37007874015748143 ) ;
#6849=EDGE_CURVE ( 'NONE', #7757, #7088, #5340, .T. ) ;
#6851=ORIENTED_EDGE ( 'NONE', *, *, #7373, .F. ) ;
#6853=ORIENTED_EDGE ( 'NONE', *, *, #1468, .T. ) ;
#6861=PLANE ( 'NONE',  #5443 ) ;
#6863=ORIENTED_EDGE ( 'NONE', *, *, #5957, .T. ) ;
#6864=AXIS2_PLACEMENT_3D ( 'NONE', #5557, #5435, #1719 ) ;
#6872=AXIS2_PLACEMENT_3D ( 'NONE', #9, #2532, #5019 ) ;
#6877=VECTOR ( 'NONE', #7763, 39.37007874015748854 ) ;
#6881=ORIENTED_EDGE ( 'NONE', *, *, #1468, .F. ) ;
#6893=AXIS2_PLACEMENT_3D ( 'NONE', #427, #7293, #6085 ) ;
#6900=ADVANCED_FACE ( 'NONE', ( #233 ), #6637, .F. ) ;
#6903=CARTESIAN_POINT ( 'NONE',  ( 3.651126735575231042, 1.000000000000000222, -1.298036422080803165 ) ) ;
#6906=CARTESIAN_POINT ( 'NONE',  ( -1.462953685906409840, 1.000000000000000222, 3.588229579118171308 ) ) ;
#6920=CARTESIAN_POINT ( 'NONE',  ( -8.751021560936518753E-10, 1.365923996832131609E-16, 5.750408897959578548E-10 ) ) ;
#6928=VERTEX_POINT ( 'NONE', #1744 ) ;
#6929=EDGE_CURVE ( 'NONE', #3899, #3397, #7301, .T. ) ;
#6949=EDGE_LOOP ( 'NONE', ( #8066, #5502 ) ) ;
#6959=CARTESIAN_POINT ( 'NONE',  ( -2.815000008655331509, 1.365923996832131609E-16, -3.895000002097408487 ) ) ;
#6960=ORIENTED_EDGE ( 'NONE', *, *, #3242, .F. ) ;
#6963=CARTESIAN_POINT ( 'NONE',  ( 3.362500000000000711, 1.750000000000000444, -4.117874862132976456E-16 ) ) ;
#6966=VERTEX_POINT ( 'NONE', #5379 ) ;
#6972=CARTESIAN_POINT ( 'NONE',  ( -8.751021560936518753E-10, 1.000000000000000222, 5.750408897959578548E-10 ) ) ;
#6981=ADVANCED_FACE ( 'NONE', ( #2364 ), #4857, .T. ) ;
#6984=EDGE_CURVE ( 'NONE', #6239, #3049, #6451, .T. ) ;
#6992=CIRCLE ( 'NONE', #5545, 0.3625000000000019318 ) ;
#6993=CARTESIAN_POINT ( 'NONE',  ( 3.562500000000000444, -0.000000000000000000, 2.975000000000000977 ) ) ;
#7003=LINE ( 'NONE', #5106, #702 ) ;
#7004=EDGE_CURVE ( 'NONE', #2549, #7021, #3862, .T. ) ;
#7015=CIRCLE ( 'NONE', #3984, 0.3625000012227142521 ) ;
#7021=VERTEX_POINT ( 'NONE', #2325 ) ;
#7025=UNCERTAINTY_MEASURE_WITH_UNIT (LENGTH_MEASURE( 1.000000000000000082E-05 ), #2479, 'distance_accuracy_value', 'NONE');
#7033=ORIENTED_EDGE ( 'NONE', *, *, #675, .T. ) ;
#7040=ORIENTED_EDGE ( 'NONE', *, *, #3929, .F. ) ;
#7042=DIRECTION ( 'NONE',  ( 0.000000000000000000, 0.000000000000000000, -1.000000000000000000 ) ) ;
#7043=FACE_OUTER_BOUND ( 'NONE', #2212, .T. ) ;
#7045=DIRECTION ( 'NONE',  ( -0.9925485533564399887, 0.000000000000000000, 0.1218497814115315075 ) ) ;
#7046=EDGE_CURVE ( 'NONE', #1701, #7088, #4535, .T. ) ;
#7050=EDGE_CURVE ( 'NONE', #5163, #1840, #6823, .T. ) ;
#7064=ORIENTED_EDGE ( 'NONE', *, *, #3211, .T. ) ;
#7080=FACE_OUTER_BOUND ( 'NONE', #6330, .T. ) ;
#7088=VERTEX_POINT ( 'NONE', #6906 ) ;
#7109=ADVANCED_FACE ( 'NONE', ( #1294 ), #6861, .F. ) ;
#7119=ORIENTED_EDGE ( 'NONE', *, *, #2792, .F. ) ;
#7128=ORIENTED_EDGE ( 'NONE', *, *, #5433, .F. ) ;
#7132=DIRECTION ( 'NONE',  ( -0.000000000000000000, -1.000000000000000000, -0.000000000000000000 ) ) ;
#7134=CARTESIAN_POINT ( 'NONE',  ( -8.751021560936518753E-10, 1.000000000000000222, 3.874999999600099443 ) ) ;
#7142=CYLINDRICAL_SURFACE ( 'NONE', #7688, 0.3625000012227142521 ) ;
#7159=EDGE_CURVE ( 'NONE', #4502, #1993, #2188, .T. ) ;
#7174=ORIENTED_EDGE ( 'NONE', *, *, #7004, .T. ) ;
#7193=CARTESIAN_POINT ( 'NONE',  ( 3.874999998766638587, 1.000000000000000222, -3.894564048797845777E-16 ) ) ;
#7206=DIRECTION ( 'NONE',  ( 0.000000000000000000, 0.000000000000000000, -1.000000000000000000 ) ) ;
#7213=ORIENTED_EDGE ( 'NONE', *, *, #5601, .F. ) ;
#7224=CARTESIAN_POINT ( 'NONE',  ( 4.470366332363715500, 1.365923996832131609E-16, 2.937534001674282358 ) ) ;
#7226=CARTESIAN_POINT ( 'NONE',  ( 3.762484563843161212, 1.281112611882646579, 0.000000000000000000 ) ) ;
#7229=CARTESIAN_POINT ( 'NONE',  ( -3.583510604133041344, 1.543025754838327046, 4.388534791062126923E-16 ) ) ;
#7234=DIRECTION ( 'NONE',  ( 0.000000000000000000, 0.000000000000000000, -1.000000000000000000 ) ) ;
#7244=VERTEX_POINT ( 'NONE', #3376 ) ;
#7257=LINE ( 'NONE', #898, #3463 ) ;
#7260=DIRECTION ( 'NONE',  ( -0.000000000000000000, 1.000000000000000000, 0.000000000000000000 ) ) ;
#7270=VECTOR ( 'NONE', #6109, 39.37007874015748143 ) ;
#7272=AXIS2_PLACEMENT_3D ( 'NONE', #3736, #6237, #5618 ) ;
#7276=CIRCLE ( 'NONE', #6864, 3.874999999025058095 ) ;
#7281=CARTESIAN_POINT ( 'NONE',  ( -3.562500000000000444, 1.000000000000000222, 2.975000000000000977 ) ) ;
#7283=CARTESIAN_POINT ( 'NONE',  ( -2.875000000000000888, -3.820994292482255198E-18, -2.975000000000000977 ) ) ;
#7293=DIRECTION ( 'NONE',  ( -0.000000000000000000, 1.000000000000000000, -0.000000000000000000 ) ) ;
#7300=DIRECTION ( 'NONE',  ( 0.000000000000000000, 0.000000000000000000, 1.000000000000000000 ) ) ;
#7301=CIRCLE ( 'NONE', #1128, 3.874999999025058095 ) ;
#7312=DIRECTION ( 'NONE',  ( -0.000000000000000000, -1.000000000000000000, -0.000000000000000000 ) ) ;
#7314=EDGE_CURVE ( 'NONE', #6365, #4981, #2262, .T. ) ;
#7323=CARTESIAN_POINT ( 'NONE',  ( 3.762484563843161656, 1.281112611882646579, 7.524969127686321535 ) ) ;
#7326=CARTESIAN_POINT ( 'NONE',  ( -3.362500000000001155, 1.750000000000000444, 4.117874862132976456E-16 ) ) ;
#7331=CARTESIAN_POINT ( 'NONE',  ( -3.791570908345035740, 1.365923996832131609E-16, 0.7997593681799630705 ) ) ;
#7345=DIRECTION ( 'NONE',  ( 0.000000000000000000, 0.000000000000000000, 1.000000000000000000 ) ) ;
#7359=CARTESIAN_POINT ( 'NONE',  ( 0.000000000000000000, 1.750000000000000444, 0.000000000000000000 ) ) ;
#7365=CARTESIAN_POINT ( 'NONE',  ( 3.875000000000001776, 1.000000000000000222, -9.491012693391993703E-16 ) ) ;
#7370=EDGE_LOOP ( 'NONE', ( #1562, #1229, #5037, #2332 ) ) ;
#7373=EDGE_CURVE ( 'NONE', #3043, #6048, #3626, .T. ) ;
#7380=EDGE_LOOP ( 'NONE', ( #6233, #6839 ) ) ;
#7382=DIRECTION ( 'NONE',  ( 0.000000000000000000, 0.000000000000000000, 1.000000000000000000 ) ) ;
#7401=EDGE_LOOP ( 'NONE', ( #2745, #3544, #5749, #5410 ) ) ;
#7403=CARTESIAN_POINT ( 'NONE',  ( 2.753607252840342579, 0.9999999999988802291, -2.731109880590252725 ) ) ;
#7408=DIRECTION ( 'NONE',  ( -0.000000000000000000, -1.000000000000000000, -0.000000000000000000 ) ) ;
#7419=LINE ( 'NONE', #7331, #3304 ) ;
#7422=AXIS2_PLACEMENT_3D ( 'NONE', #5580, #4844, #6695 ) ;
#7425=VECTOR ( 'NONE', #2172, 39.37007874015748143 ) ;
#7431=DIRECTION ( 'NONE',  ( 0.000000000000000000, 0.000000000000000000, -1.000000000000000000 ) ) ;
#7443=CARTESIAN_POINT ( 'NONE',  ( 3.362500000000000711, 1.750000000000000444, -4.117874862132976456E-16 ) ) ;
#7446=AXIS2_PLACEMENT_3D ( 'NONE', #4191, #3592, #7382 ) ;
#7448=CIRCLE ( 'NONE', #4925, 0.3625000012227142521 ) ;
#7451=DIRECTION ( 'NONE',  ( -0.000000000000000000, -1.000000000000000000, -0.000000000000000000 ) ) ;
#7453=LINE ( 'NONE', #1187, #5945 ) ;
#7464=DIRECTION ( 'NONE',  ( 0.000000000000000000, 0.000000000000000000, -1.000000000000000000 ) ) ;
#7465=FACE_OUTER_BOUND ( 'NONE', #517, .T. ) ;
#7472=EDGE_CURVE ( 'NONE', #3397, #4502, #7419, .T. ) ;
#7491=FACE_OUTER_BOUND ( 'NONE', #2856, .T. ) ;
#7498=ORIENTED_EDGE ( 'NONE', *, *, #7472, .F. ) ;
#7499=CARTESIAN_POINT ( 'NONE',  ( 3.484120143574221651E-16, 0.000000000000000000, 2.845000000000001528 ) ) ;
#7525=ADVANCED_FACE ( 'NONE', ( #3190 ), #3066, .F. ) ;
#7530=CARTESIAN_POINT ( 'NONE',  ( -8.751021560936518753E-10, 1.000000000000000222, 5.750408897959578548E-10 ) ) ;
#7532=DIRECTION ( 'NONE',  ( 0.000000000000000000, 0.000000000000000000, 1.000000000000000000 ) ) ;
#7550=VECTOR ( 'NONE', #6655, 39.37007874015748143 ) ;
#7554=VECTOR ( 'NONE', #3152, 39.37007874015748143 ) ;
#7559=VECTOR ( 'NONE', #4027, 39.37007874015748143 ) ;
#7571=EDGE_LOOP ( 'NONE', ( #2775, #535, #4960, #355 ) ) ;
#7573=ADVANCED_FACE ( 'NONE', ( #6308, #4915 ), #652, .T. ) ;
#7581=DIRECTION ( 'NONE',  ( 0.000000000000000000, -0.000000000000000000, 1.000000000000000000 ) ) ;
#7582=AXIS2_PLACEMENT_3D ( 'NONE', #2159, #930, #6425 ) ;
#7587=EDGE_CURVE ( 'NONE', #1938, #5712, #3962, .T. ) ;
#7591=VERTEX_POINT ( 'NONE', #6959 ) ;
#7592=VECTOR ( 'NONE', #1191, 39.37007874015748143 ) ;
#7600=DIRECTION ( 'NONE',  ( 0.3026345437736693289, 0.000000000000000000, -0.9531066744677130220 ) ) ;
#7601=ORIENTED_EDGE ( 'NONE', *, *, #784, .F. ) ;
#7603=LINE ( 'NONE', #1954, #4644 ) ;
#7606=FACE_BOUND ( 'NONE', #3723, .T. ) ;
#7612=ORIENTED_EDGE ( 'NONE', *, *, #6553, .T. ) ;
#7619=DIRECTION ( 'NONE',  ( 0.000000000000000000, 1.000000000000000000, 0.000000000000000000 ) ) ;
#7624=ORIENTED_EDGE ( 'NONE', *, *, #317, .F. ) ;
#7637=EDGE_LOOP ( 'NONE', ( #3638, #7826 ) ) ;
#7642=DIRECTION ( 'NONE',  ( -0.000000000000000000, 1.000000000000000000, 0.000000000000000000 ) ) ;
#7649=EDGE_LOOP ( 'NONE', ( #1460, #7601, #6158, #1818, #174, #809, #5518, #7119, #6116, #1223, #2442, #6705, #4236, #3028, #3982, #5772, #5178 ) ) ;
#7656=PLANE ( 'NONE',  #5015 ) ;
#7657=( LENGTH_UNIT ( ) NAMED_UNIT ( * ) SI_UNIT ( $, .METRE. ) );
#7659=ORIENTED_EDGE ( 'NONE', *, *, #7314, .F. ) ;
#7664=AXIS2_PLACEMENT_3D ( 'NONE', #969, #1738, #3038 ) ;
#7666=CARTESIAN_POINT ( 'NONE',  ( 0.000000000000000000, 0.000000000000000000, -2.845000000000001528 ) ) ;
#7683=FACE_OUTER_BOUND ( 'NONE', #1039, .T. ) ;
#7688=AXIS2_PLACEMENT_3D ( 'NONE', #4012, #5321, #1566 ) ;
#7703=CIRCLE ( 'NONE', #2690, 0.3625000000000019318 ) ;
#7707=AXIS2_PLACEMENT_3D ( 'NONE', #5128, #3334, #5956 ) ;
#7711=ORIENTED_EDGE ( 'NONE', *, *, #6059, .T. ) ;
#7718=ORIENTED_EDGE ( 'NONE', *, *, #601, .F. ) ;
#7719=DIRECTION ( 'NONE',  ( -0.000000000000000000, 1.000000000000000000, -0.000000000000000000 ) ) ;
#7723=VERTEX_POINT ( 'NONE', #6127 ) ;
#7748=ORIENTED_EDGE ( 'NONE', *, *, #388, .F. ) ;
#7757=VERTEX_POINT ( 'NONE', #2359 ) ;
#7760=CYLINDRICAL_SURFACE ( 'NONE', #4234, 3.874999999025058539 ) ;
#7763=DIRECTION ( 'NONE',  ( 0.9917930140139561423, -0.000000000000000000, -0.1278538906451907597 ) ) ;
#7774=( BOUNDED_SURFACE ( )  B_SPLINE_SURFACE ( 3, 3, ( 
 ( #2388, #4713, #6693, #7365 ),
 ( #459, #5403, #4209, #1692 ),
 ( #7963, #2303, #3617, #4749 ),
 ( #999, #8051, #2955, #6115 ) ),
 .UNSPECIFIED., .F., .F., .T. ) 
 B_SPLINE_SURFACE_WITH_KNOTS ( ( 4, 4 ),
 ( 4, 4 ),
 ( 0.000000000000000000, 1.000000000000000000 ),
 ( 0.000000000000000000, 1.000000000000000000 ),
 .UNSPECIFIED. ) 
 GEOMETRIC_REPRESENTATION_ITEM ( )  RATIONAL_B_SPLINE_SURFACE ( (
 ( 1.000000000000000000, 0.3333333333333334259, 0.3333333333333334259, 1.000000000000000000),
 ( 1.000000000000000000, 0.3333333333333334259, 0.3333333333333334259, 1.000000000000000000),
 ( 1.000000000000000000, 0.3333333333333334259, 0.3333333333333334259, 1.000000000000000000),
 ( 1.000000000000000000, 0.3333333333333334259, 0.3333333333333334259, 1.000000000000000000) ) ) 
 REPRESENTATION_ITEM ( '' )  SURFACE ( )  );
#7823=CARTESIAN_POINT ( 'NONE',  ( 3.791570905984167794, 1.365923996832131609E-16, 0.7997593710750563467 ) ) ;
#7824=CIRCLE ( 'NONE', #1762, 0.3625000000000019318 ) ;
#7826=ORIENTED_EDGE ( 'NONE', *, *, #6650, .F. ) ;
#7827=AXIS2_PLACEMENT_3D ( 'NONE', #4737, #7132, #6646 ) ;
#7833=FACE_OUTER_BOUND ( 'NONE', #2244, .T. ) ;
#7836=EDGE_LOOP ( 'NONE', ( #2240, #7064, #5046, #8122 ) ) ;
#7843=DIRECTION ( 'NONE',  ( -0.9925485533740563415, 0.000000000000000000, -0.1218497812680346959 ) ) ;
#7848=AXIS2_PLACEMENT_3D ( 'NONE', #4026, #4683, #3086 ) ;
#7854=CARTESIAN_POINT ( 'NONE',  ( -8.751021560936518753E-10, 1.365923996832131609E-16, 5.750408897959578548E-10 ) ) ;
#7870=CYLINDRICAL_SURFACE ( 'NONE', #6349, 4.805751768934915624 ) ;
#7873=ORIENTED_EDGE ( 'NONE', *, *, #2836, .T. ) ;
#7892=CARTESIAN_POINT ( 'NONE',  ( -8.751021560936518753E-10, 1.365923996832131609E-16, 5.750408897959578548E-10 ) ) ;
#7895=ORIENTED_EDGE ( 'NONE', *, *, #7587, .F. ) ;
#7900=ORIENTED_EDGE ( 'NONE', *, *, #6093, .F. ) ;
#7908=DIRECTION ( 'NONE',  ( -0.000000000000000000, 1.000000000000000000, 0.000000000000000000 ) ) ;
#7909=SHAPE_DEFINITION_REPRESENTATION ( #6474, #4813 ) ;
#7916=CARTESIAN_POINT ( 'NONE',  ( 3.583510604133040900, 1.543025754838326824, 7.167021208266081800 ) ) ;
#7925=VERTEX_POINT ( 'NONE', #4599 ) ;
#7928=EDGE_CURVE ( 'NONE', #3049, #6239, #1467, .T. ) ;
#7936=AXIS2_PLACEMENT_3D ( 'NONE', #5567, #7451, #3798 ) ;
#7943=ORIENTED_EDGE ( 'NONE', *, *, #7373, .T. ) ;
#7955=DIRECTION ( 'NONE',  ( 0.000000000000000000, 0.000000000000000000, -1.000000000000000000 ) ) ;
#7963=CARTESIAN_POINT ( 'NONE',  ( -3.583510604133041344, 1.543025754838327046, 4.388534791062126923E-16 ) ) ;
#7972=CARTESIAN_POINT ( 'NONE',  ( 2.875000000000000888, 1.000000000000000222, -2.975000000000000977 ) ) ;
#7985=CIRCLE ( 'NONE', #7707, 0.3625000012227142521 ) ;
#7991=CIRCLE ( 'NONE', #6893, 5.349138356872925826 ) ;
#7992=EDGE_CURVE ( 'NONE', #5154, #2528, #2409, .T. ) ;
#7995=ORIENTED_EDGE ( 'NONE', *, *, #4125, .T. ) ;
#7997=DIRECTION ( 'NONE',  ( 0.000000000000000000, 0.000000000000000000, -1.000000000000000000 ) ) ;
#7998=CARTESIAN_POINT ( 'NONE',  ( 2.875000000000000888, 1.000000000000000222, -2.975000000000000977 ) ) ;
#8008=DIRECTION ( 'NONE',  ( 0.000000000000000000, 0.000000000000000000, -1.000000000000000000 ) ) ;
#8016=EDGE_CURVE ( 'NONE', #2186, #295, #5551, .T. ) ;
#8017=CARTESIAN_POINT ( 'NONE',  ( -3.651126736336024248, 1.000000000000000444, -1.298036422402331302 ) ) ;
#8029=DIRECTION ( 'NONE',  ( 0.000000000000000000, 0.000000000000000000, 1.000000000000000000 ) ) ;
#8048=CARTESIAN_POINT ( 'NONE',  ( -3.362500000000001155, 1.750000000000000444, 4.117874862132976456E-16 ) ) ;
#8050=ORIENTED_EDGE ( 'NONE', *, *, #7004, .F. ) ;
#8051=CARTESIAN_POINT ( 'NONE',  ( -3.362500000000002931, 1.750000000000000222, -6.725000000000002309 ) ) ;
#8053=EDGE_LOOP ( 'NONE', ( #1892, #2049, #5819, #7995, #2805 ) ) ;
#8057=ORIENTED_EDGE ( 'NONE', *, *, #7992, .F. ) ;
#8066=ORIENTED_EDGE ( 'NONE', *, *, #5998, .T. ) ;
#8071=FACE_OUTER_BOUND ( 'NONE', #5002, .T. ) ;
#8079=EDGE_CURVE ( 'NONE', #7925, #1840, #537, .T. ) ;
#8081=AXIS2_PLACEMENT_3D ( 'NONE', #3794, #7642, #729 ) ;
#8083=CARTESIAN_POINT ( 'NONE',  ( 1.172489671196043304, 1.000000000000000444, -3.693357952326151494 ) ) ;
#8090=CARTESIAN_POINT ( 'NONE',  ( 2.637478091534485092, 0.9999999999988804511, -2.843572666449059927 ) ) ;
#8092=VERTEX_POINT ( 'NONE', #6119 ) ;
#8106=AXIS2_PLACEMENT_3D ( 'NONE', #3194, #5691, #1560 ) ;
#8113=DIRECTION ( 'NONE',  ( 0.000000000000000000, 0.000000000000000000, 1.000000000000000000 ) ) ;
#8119=FACE_OUTER_BOUND ( 'NONE', #2823, .T. ) ;
#8121=FACE_OUTER_BOUND ( 'NONE', #5881, .T. ) ;
#8122=ORIENTED_EDGE ( 'NONE', *, *, #2537, .T. ) ;
#8131=ORIENTED_EDGE ( 'NONE', *, *, #743, .T. ) ;
#8134=LINE ( 'NONE', #4871, #191 ) ;
#8139=VERTEX_POINT ( 'NONE', #5701 ) ;
#8160=CYLINDRICAL_SURFACE ( 'NONE', #5988, 0.3625000012227142521 ) ;
#8171=DIRECTION ( 'NONE',  ( 0.000000000000000000, 1.000000000000000000, 0.000000000000000000 ) ) ;
#8227=COLOUR_RGB('Light Gray', 0.08235294, 0.09019608, 0.10196078);
#8228=FILL_AREA_STYLE_COLOUR('',#8227);
#8229=FILL_AREA_STYLE('',(#8228));
#8230=SURFACE_STYLE_FILL_AREA(#8229);
#8231=SURFACE_SIDE_STYLE('',(#8230));
#8232=SURFACE_STYLE_USAGE(.BOTH.,#8231);
#8233=PRESENTATION_STYLE_ASSIGNMENT((#8232));
#8243=STYLED_ITEM('',(#8233),#4597);
#8244=MECHANICAL_DESIGN_GEOMETRIC_PRESENTATION_REPRESENTATION('',(#8243),#3062);
ENDSEC;
END-ISO-10303-21;
